ISO-10303-21;
HEADER;
FILE_DESCRIPTION (('STEP AP214'),
    '1' );
FILE_NAME ('hex nut gradec_bsi_BS EN 24034 - M5 - N.step',
    '2026-10-06T08:09:25',
    ( '' ),
    ( '' ),
    'SwSTEP 2.0',
    'SolidWorks 2021',
    '' );
FILE_SCHEMA (( 'AUTOMOTIVE_DESIGN' ));
ENDSEC;

DATA;
#1=CARTESIAN_POINT ( 'NONE',  ( 2.099999999999999645, 0.000000000000000000, -5.294516984716112873 ) ) ;
#36=CARTESIAN_POINT ( 'NONE',  ( 0.000000000000000000, 0.000000000000000000, -5.600000000000000533 ) ) ;
#59=ORIENTED_EDGE ( 'NONE', *, *, #18406, .T. ) ;
#136=AXIS2_PLACEMENT_3D ( 'NONE', #2395, #9803, #3063 ) ;
#143=EDGE_LOOP ( 'NONE', ( #667, #18574, #6068, #5287 ) ) ;
#175=ORIENTED_EDGE ( 'NONE', *, *, #6794, .T. ) ;
#198=FACE_OUTER_BOUND ( 'NONE', #17875, .T. ) ;
#258=FACE_OUTER_BOUND ( 'NONE', #543, .T. ) ;
#266=CARTESIAN_POINT ( 'NONE',  ( 1.660531772554329821, -3.660093687634887072, -5.599999999999980105 ) ) ;
#321=B_SPLINE_CURVE_WITH_KNOTS ( 'NONE', 3,
 ( #20102, #14913, #7632, #14569 ),
 .UNSPECIFIED., .F., .F.,
 ( 4, 4 ),
 ( 2.380737582390834275E-07, 0.002336974151641598059 ),
 .UNSPECIFIED. ) ;
#357=STYLED_ITEM ( 'NONE', ( #13468 ), #10311 ) ;
#381=DIRECTION ( 'NONE',  ( 0.8660254037844354880, -0.5000000000000055511, 0.000000000000000000 ) ) ;
#387=CARTESIAN_POINT ( 'NONE',  ( 1.387778780781445676E-14, 4.618802153517020059, -0.3572655899081733644 ) ) ;
#419=CARTESIAN_POINT ( 'NONE',  ( 0.000000000000000000, 0.000000000000000000, -25.03750572909317285 ) ) ;
#421=ORIENTED_EDGE ( 'NONE', *, *, #13406, .T. ) ;
#517=AXIS2_PLACEMENT_3D ( 'NONE', #18682, #14064, #6345 ) ;
#543=EDGE_LOOP ( 'NONE', ( #12301, #5370, #12717, #13469, #20277, #9943 ) ) ;
#604=LINE ( 'NONE', #834, #21874 ) ;
#612=CARTESIAN_POINT ( 'NONE',  ( -1.660531772554314722, 3.660093687634845772, -5.600000000000003197 ) ) ;
#625=CIRCLE ( 'NONE', #16019, 2.500000000000000444 ) ;
#667=ORIENTED_EDGE ( 'NONE', *, *, #10371, .T. ) ;
#679=EDGE_CURVE ( 'NONE', #5232, #20512, #15973, .T. ) ;
#715=CIRCLE ( 'NONE', #5215, 3.999999999999999112 ) ;
#727=LINE ( 'NONE', #18828, #3425 ) ;
#738=B_SPLINE_CURVE_WITH_KNOTS ( 'NONE', 3,
 ( #10637, #10409, #16039, #1817 ),
 .UNSPECIFIED., .F., .F.,
 ( 4, 4 ),
 ( 2.380737581550306806E-07, 0.002336974151641528670 ),
 .UNSPECIFIED. ) ;
#769=CARTESIAN_POINT ( 'NONE',  ( 0.000000000000000000, 0.000000000000000000, -5.600000000000000533 ) ) ;
#796=CARTESIAN_POINT ( 'NONE',  ( -6.938893903907228378E-14, -4.618802153517020059, -5.242734410091827613 ) ) ;
#824=DIRECTION ( 'NONE',  ( 0.8191520442889927978, 1.003171929053525979E-16, -0.5735764363510447161 ) ) ;
#834=CARTESIAN_POINT ( 'NONE',  ( 4.000000000000003553, -2.309401076758539784, -5.600000000000000533 ) ) ;
#850=CARTESIAN_POINT ( 'NONE',  ( 0.000000000000000000, 0.000000000000000000, -5.600000000000000533 ) ) ;
#858=ORIENTED_EDGE ( 'NONE', *, *, #16843, .T. ) ;
#867=AXIS2_PLACEMENT_3D ( 'NONE', #14945, #4006, #381 ) ;
#902=VERTEX_POINT ( 'NONE', #14802 ) ;
#912=EDGE_CURVE ( 'NONE', #21589, #16716, #321, .T. ) ;
#916=CARTESIAN_POINT ( 'NONE',  ( 2.060000000000002718, 0.000000000000000000, -0.3080913168122707546 ) ) ;
#1045=DIRECTION ( 'NONE',  ( 0.000000000000000000, -0.000000000000000000, 1.000000000000000000 ) ) ;
#1072=VERTEX_POINT ( 'NONE', #4438 ) ;
#1080=EDGE_CURVE ( 'NONE', #3914, #9423, #17915, .T. ) ;
#1131=VERTEX_POINT ( 'NONE', #3036 ) ;
#1148=VERTEX_POINT ( 'NONE', #23035 ) ;
#1176=EDGE_LOOP ( 'NONE', ( #59, #15142, #15367 ) ) ;
#1213=CARTESIAN_POINT ( 'NONE',  ( -4.000000000000003553, 0.000000000000000000, 0.000000000000000000 ) ) ;
#1260=DIRECTION ( 'NONE',  ( 1.000000000000000000, 0.000000000000000000, 0.000000000000000000 ) ) ;
#1261=VECTOR ( 'NONE', #12249, 1000.000000000000000 ) ;
#1265=CARTESIAN_POINT ( 'NONE',  ( 2.099999999999999645, 0.000000000000000000, -5.600000000000000533 ) ) ;
#1283=CARTESIAN_POINT ( 'NONE',  ( -2.500000000000002220, 3.061616997868386099E-16, -5.600000000000000533 ) ) ;
#1293=CARTESIAN_POINT ( 'NONE',  ( 0.000000000000000000, 0.000000000000000000, -5.600000000000000533 ) ) ;
#1297=ORIENTED_EDGE ( 'NONE', *, *, #12754, .F. ) ;
#1345=EDGE_CURVE ( 'NONE', #1131, #5232, #18083, .T. ) ;
#1367=CARTESIAN_POINT ( 'NONE',  ( 4.000000000000004441, -1.549102112939114484, -5.442104661404057353 ) ) ;
#1406=ORIENTED_EDGE ( 'NONE', *, *, #11534, .F. ) ;
#1488=ADVANCED_FACE ( 'NONE', ( #15553 ), #13794, .F. ) ;
#1491=CONICAL_SURFACE ( 'NONE', #1847, 4.000000000000000000, 1.047197551196595855 ) ;
#1538=CARTESIAN_POINT ( 'NONE',  ( 2.000000000000029310, 3.464101615137740175, 0.000000000000000000 ) ) ;
#1545=ORIENTED_EDGE ( 'NONE', *, *, #22875, .F. ) ;
#1569=ORIENTED_EDGE ( 'NONE', *, *, #7673, .F. ) ;
#1704=AXIS2_PLACEMENT_3D ( 'NONE', #17732, #23164, #21278 ) ;
#1721=ORIENTED_EDGE ( 'NONE', *, *, #4503, .F. ) ;
#1755=CARTESIAN_POINT ( 'NONE',  ( 0.000000000000000000, 0.000000000000000000, -5.600000000000000533 ) ) ;
#1786=CARTESIAN_POINT ( 'NONE',  ( 3.999999999999989786, -2.309401076758549998, -0.3572655899081733644 ) ) ;
#1817=CARTESIAN_POINT ( 'NONE',  ( -2.000000000000015543, 3.464101615137746837, 0.000000000000000000 ) ) ;
#1847=AXIS2_PLACEMENT_3D ( 'NONE', #21299, #15754, #15635 ) ;
#1849=CARTESIAN_POINT ( 'NONE',  ( -4.000000000000003553, -2.309401076758525573, -5.600000000000000533 ) ) ;
#1881=ORIENTED_EDGE ( 'NONE', *, *, #6149, .T. ) ;
#1885=ORIENTED_EDGE ( 'NONE', *, *, #15397, .T. ) ;
#1901=CARTESIAN_POINT ( 'NONE',  ( -6.938893903907228378E-14, -4.618802153517020059, -5.242734410091827613 ) ) ;
#1906=ORIENTED_EDGE ( 'NONE', *, *, #10371, .F. ) ;
#1948=CARTESIAN_POINT ( 'NONE',  ( 2.500000000000002220, 0.000000000000000000, -25.03750572909317285 ) ) ;
#1975=AXIS2_PLACEMENT_3D ( 'NONE', #8643, #15800, #4991 ) ;
#2029=CONICAL_SURFACE ( 'NONE', #11049, 4.000000000000000000, 1.047197551196595855 ) ;
#2052=DIRECTION ( 'NONE',  ( -0.000000000000000000, -0.000000000000000000, 1.000000000000000000 ) ) ;
#2072=ADVANCED_FACE ( 'NONE', ( #5996 ), #15152, .F. ) ;
#2180=EDGE_CURVE ( 'NONE', #20512, #5232, #6304, .T. ) ;
#2205=CARTESIAN_POINT ( 'NONE',  ( -2.000000000000015543, -3.464101615137743728, 0.000000000000000000 ) ) ;
#2227=MECHANICAL_DESIGN_GEOMETRIC_PRESENTATION_REPRESENTATION('',(#357),#13500);
#2250=CARTESIAN_POINT ( 'NONE',  ( 1.387778780781445676E-14, 4.618802153517020059, -5.242734410091827613 ) ) ;
#2257=DIRECTION ( 'NONE',  ( -1.000000000000000000, 0.000000000000000000, 0.000000000000000000 ) ) ;
#2262=VERTEX_POINT ( 'NONE', #1283 ) ;
#2268=ORIENTED_EDGE ( 'NONE', *, *, #21470, .T. ) ;
#2333=DIRECTION ( 'NONE',  ( 1.000000000000000000, 0.000000000000000000, 0.000000000000000000 ) ) ;
#2339=ADVANCED_FACE ( 'NONE', ( #21275 ), #21736, .T. ) ;
#2347=AXIS2_PLACEMENT_3D ( 'NONE', #6449, #1045, #11728 ) ;
#2367=FACE_OUTER_BOUND ( 'NONE', #14508, .T. ) ;
#2370=CONICAL_SURFACE ( 'NONE', #17389, 4.000000000000000000, 1.047197551196595855 ) ;
#2375=EDGE_LOOP ( 'NONE', ( #6187, #5584, #1906, #1569 ) ) ;
#2387=CONICAL_SURFACE ( 'NONE', #15529, 4.000000000000000000, 1.047197551196595855 ) ;
#2395=CARTESIAN_POINT ( 'NONE',  ( 0.000000000000000000, 0.000000000000000000, -0.3080913168122707546 ) ) ;
#2403=EDGE_CURVE ( 'NONE', #17189, #18558, #15703, .T. ) ;
#2412=ORIENTED_EDGE ( 'NONE', *, *, #7948, .T. ) ;
#2429=B_SPLINE_CURVE_WITH_KNOTS ( 'NONE', 3,
 ( #4016, #266, #14845, #22018, #20029, #1901 ),
 .UNSPECIFIED., .F., .F.,
 ( 4, 2, 4 ),
 ( 0.002336974151641522165, 0.003500975885716451491, 0.004664977619791380384 ),
 .UNSPECIFIED. ) ;
#2444=CARTESIAN_POINT ( 'NONE',  ( -4.000000000000004441, -1.549102112939104714, -5.442104661404059129 ) ) ;
#2519=UNCERTAINTY_MEASURE_WITH_UNIT (LENGTH_MEASURE( 1.000000000000000082E-05 ), #17091, 'distance_accuracy_value', 'NONE');
#2551=AXIS2_PLACEMENT_3D ( 'NONE', #15228, #8069, #16879 ) ;
#2564=CARTESIAN_POINT ( 'NONE',  ( 1.387778780781445676E-14, 4.618802153517020059, -5.600000000000000533 ) ) ;
#2596=DIRECTION ( 'NONE',  ( 1.000000000000000000, 0.000000000000000000, 0.000000000000000000 ) ) ;
#2637=ADVANCED_FACE ( 'NONE', ( #16988 ), #8429, .F. ) ;
#2723=ADVANCED_FACE ( 'NONE', ( #13719 ), #20984, .F. ) ;
#2778=CARTESIAN_POINT ( 'NONE',  ( 0.000000000000000000, 0.000000000000000000, -5.600000000000000533 ) ) ;
#2782=PLANE ( 'NONE',  #19125 ) ;
#2808=LINE ( 'NONE', #2564, #11716 ) ;
#2835=CARTESIAN_POINT ( 'NONE',  ( 2.000000000000029310, 3.464101615137740175, -5.600000000000000533 ) ) ;
#2846=AXIS2_PLACEMENT_3D ( 'NONE', #3096, #8277, #20868 ) ;
#2859=CARTESIAN_POINT ( 'NONE',  ( -2.500000000000000444, 3.061616997868383634E-16, 3.415236843329338967E-15 ) ) ;
#2881=CARTESIAN_POINT ( 'NONE',  ( 4.000000000000003553, 2.309401076758525573, -5.242734410091827613 ) ) ;
#2900=EDGE_CURVE ( 'NONE', #6499, #9593, #16822, .T. ) ;
#2929=CARTESIAN_POINT ( 'NONE',  ( 2.000000000000029310, 3.464101615137740175, 0.000000000000000000 ) ) ;
#2955=CARTESIAN_POINT ( 'NONE',  ( -2.000000000000015543, -3.464101615137743728, -5.600000000000000533 ) ) ;
#2963=DIRECTION ( 'NONE',  ( 0.000000000000000000, 0.000000000000000000, 1.000000000000000000 ) ) ;
#2984=CARTESIAN_POINT ( 'NONE',  ( 3.999999999999989786, -2.309401076758549998, -5.242734410091827613 ) ) ;
#2988=( GEOMETRIC_REPRESENTATION_CONTEXT ( 3 ) GLOBAL_UNCERTAINTY_ASSIGNED_CONTEXT ( ( #2519 ) ) GLOBAL_UNIT_ASSIGNED_CONTEXT ( ( #17091, #13586, #9942 ) ) REPRESENTATION_CONTEXT ( 'NONE', 'WORKASPACE' ) );
#3006=DIRECTION ( 'NONE',  ( 0.8660254037844371533, 0.5000000000000025535, 0.000000000000000000 ) ) ;
#3036=CARTESIAN_POINT ( 'NONE',  ( 2.500000000000002220, 0.000000000000000000, -5.600000000000000533 ) ) ;
#3047=CARTESIAN_POINT ( 'NONE',  ( 1.387778780781445676E-14, 4.618802153517020059, -0.3572655899081733644 ) ) ;
#3063=DIRECTION ( 'NONE',  ( 1.000000000000000000, 0.000000000000000000, 0.000000000000000000 ) ) ;
#3079=EDGE_CURVE ( 'NONE', #7097, #4023, #18164, .T. ) ;
#3096=CARTESIAN_POINT ( 'NONE',  ( 0.000000000000000000, 0.000000000000000000, -25.03750572909317285 ) ) ;
#3119=ORIENTED_EDGE ( 'NONE', *, *, #13675, .F. ) ;
#3130=CARTESIAN_POINT ( 'NONE',  ( 4.000000000000003553, -1.933795701539624323, -5.351162342337697275 ) ) ;
#3135=( LENGTH_UNIT ( ) NAMED_UNIT ( * ) SI_UNIT ( .MILLI., .METRE. ) );
#3178=ORIENTED_EDGE ( 'NONE', *, *, #4244, .F. ) ;
#3188=ORIENTED_EDGE ( 'NONE', *, *, #5833, .T. ) ;
#3227=FACE_BOUND ( 'NONE', #18498, .T. ) ;
#3265=ORIENTED_EDGE ( 'NONE', *, *, #6149, .F. ) ;
#3336=VECTOR ( 'NONE', #22675, 1000.000000000000000 ) ;
#3343=DIRECTION ( 'NONE',  ( 1.000000000000000000, 0.000000000000000000, 0.000000000000000000 ) ) ;
#3373=CARTESIAN_POINT ( 'NONE',  ( 4.000000000000003553, 1.935983797701079423, -5.350530693383767300 ) ) ;
#3425=VECTOR ( 'NONE', #18709, 1000.000000000000000 ) ;
#3446=DIRECTION ( 'NONE',  ( -0.000000000000000000, -0.000000000000000000, 1.000000000000000000 ) ) ;
#3542=CARTESIAN_POINT ( 'NONE',  ( -4.000000000000003553, -2.309401076758532678, -0.3572655899081733644 ) ) ;
#3586=CARTESIAN_POINT ( 'NONE',  ( 4.000000000000003553, 0.3904826640788058856, -2.016361930938861168E-15 ) ) ;
#3597=DIRECTION ( 'NONE',  ( -1.000000000000000000, 0.000000000000000000, 0.000000000000000000 ) ) ;
#3612=CARTESIAN_POINT ( 'NONE',  ( 2.000000000000015543, -3.464101615137746837, 0.000000000000000000 ) ) ;
#3626=DIRECTION ( 'NONE',  ( -0.000000000000000000, -0.000000000000000000, 1.000000000000000000 ) ) ;
#3676=B_SPLINE_CURVE_WITH_KNOTS ( 'NONE', 3,
 ( #4679, #8449, #13506, #17363 ),
 .UNSPECIFIED., .F., .F.,
 ( 4, 4 ),
 ( 2.380737582390371584E-07, 0.002336974151641598059 ),
 .UNSPECIFIED. ) ;
#3693=ORIENTED_EDGE ( 'NONE', *, *, #14747, .F. ) ;
#3699=CARTESIAN_POINT ( 'NONE',  ( 0.000000000000000000, 0.000000000000000000, 0.000000000000000000 ) ) ;
#3762=PRODUCT_CONTEXT ( 'NONE', #14336, 'mechanical' ) ;
#3780=CARTESIAN_POINT ( 'NONE',  ( 4.000000000000003553, 0.3904826640788060521, -5.599999999999997868 ) ) ;
#3796=EDGE_CURVE ( 'NONE', #12394, #7255, #8541, .T. ) ;
#3801=B_SPLINE_CURVE_WITH_KNOTS ( 'NONE', 3,
 ( #14316, #10551, #21036, #3612 ),
 .UNSPECIFIED., .F., .F.,
 ( 4, 4 ),
 ( 2.380737581852354520E-07, 0.002336974151641521731 ),
 .UNSPECIFIED. ) ;
#3802=ORIENTED_EDGE ( 'NONE', *, *, #19762, .F. ) ;
#3819=ORIENTED_EDGE ( 'NONE', *, *, #11690, .F. ) ;
#3904=ADVANCED_FACE ( 'NONE', ( #11709 ), #2782, .T. ) ;
#3914=VERTEX_POINT ( 'NONE', #4881 ) ;
#3923=CARTESIAN_POINT ( 'NONE',  ( 4.000000000000003553, 1.935983797701078757, -0.2494693066162351203 ) ) ;
#3940=UNCERTAINTY_MEASURE_WITH_UNIT (LENGTH_MEASURE( 1.000000000000000082E-05 ), #22291, 'distance_accuracy_value', 'NONE');
#3941=DIRECTION ( 'NONE',  ( -0.000000000000000000, -0.000000000000000000, 1.000000000000000000 ) ) ;
#3994=EDGE_LOOP ( 'NONE', ( #19954, #15374, #12009 ) ) ;
#4006=DIRECTION ( 'NONE',  ( -0.5000000000000055511, -0.8660254037844354880, 0.000000000000000000 ) ) ;
#4014=FACE_OUTER_BOUND ( 'NONE', #5435, .T. ) ;
#4016=CARTESIAN_POINT ( 'NONE',  ( 2.000000000000015543, -3.464101615137746837, -5.600000000000000533 ) ) ;
#4023=VERTEX_POINT ( 'NONE', #16046 ) ;
#4086=ADVANCED_FACE ( 'NONE', ( #13224 ), #14204, .F. ) ;
#4124=CONICAL_SURFACE ( 'NONE', #13894, 4.000000000000000000, 1.047197551196595855 ) ;
#4127=PLANE ( 'NONE',  #18459 ) ;
#4148=FACE_OUTER_BOUND ( 'NONE', #16917, .T. ) ;
#4192=CARTESIAN_POINT ( 'NONE',  ( -4.000000000000003553, -1.933795701539609446, -5.351162342337700828 ) ) ;
#4230=CARTESIAN_POINT ( 'NONE',  ( -0.3263565795980838957, 4.430380094434251959, -5.351519936624994145 ) ) ;
#4244=EDGE_CURVE ( 'NONE', #18520, #6499, #15342, .T. ) ;
#4267=CARTESIAN_POINT ( 'NONE',  ( -2.000000000000015543, -3.464101615137743728, -5.600000000000000533 ) ) ;
#4268=DIRECTION ( 'NONE',  ( -0.000000000000000000, -0.000000000000000000, 1.000000000000000000 ) ) ;
#4309=ORIENTED_EDGE ( 'NONE', *, *, #2900, .F. ) ;
#4320=CARTESIAN_POINT ( 'NONE',  ( 0.000000000000000000, 0.000000000000000000, -5.574599999999999334 ) ) ;
#4324=FACE_OUTER_BOUND ( 'NONE', #14131, .T. ) ;
#4350=CARTESIAN_POINT ( 'NONE',  ( -0.6554360035617893265, 4.240386000424037682, -0.1586754815284909248 ) ) ;
#4376=CARTESIAN_POINT ( 'NONE',  ( 0.000000000000000000, 0.000000000000000000, -0.2800830152838856835 ) ) ;
#4381=CARTESIAN_POINT ( 'NONE',  ( 3.345653888883671989, -2.687187980154742473, -5.460849780464843484 ) ) ;
#4420=CARTESIAN_POINT ( 'NONE',  ( 0.000000000000000000, 0.000000000000000000, 3.469446951953614189E-15 ) ) ;
#4438=CARTESIAN_POINT ( 'NONE',  ( 4.000000000000003553, 0.000000000000000000, -5.600000000000000533 ) ) ;
#4460=B_SPLINE_CURVE_WITH_KNOTS ( 'NONE', 3,
 ( #15057, #22250, #13315, #4350, #18715, #387 ),
 .UNSPECIFIED., .F., .F.,
 ( 4, 2, 4 ),
 ( 0.002336974151641528670, 0.003500975885716446721, 0.004664977619791364771 ),
 .UNSPECIFIED. ) ;
#4478=CARTESIAN_POINT ( 'NONE',  ( -2.678494666091062015, -3.072372537026391459, -5.565789719053451101 ) ) ;
#4503=EDGE_CURVE ( 'NONE', #4023, #21589, #2429, .T. ) ;
#4505=CARTESIAN_POINT ( 'NONE',  ( 3.673643420401898840, 2.497823135841254150, -0.2484800633749945087 ) ) ;
#4542=DIRECTION ( 'NONE',  ( -0.000000000000000000, -0.000000000000000000, 1.000000000000000000 ) ) ;
#4547=ADVANCED_FACE ( 'NONE', ( #18041 ), #13401, .T. ) ;
#4593=CARTESIAN_POINT ( 'NONE',  ( 0.000000000000000000, 0.000000000000000000, -5.600000000000000533 ) ) ;
#4631=AXIS2_PLACEMENT_3D ( 'NONE', #8571, #3626, #17621 ) ;
#4632=FILL_AREA_STYLE ('',( #22526 ) ) ;
#4651=CARTESIAN_POINT ( 'NONE',  ( 4.000000000000003553, 2.309401076758525573, -5.242734410091827613 ) ) ;
#4679=CARTESIAN_POINT ( 'NONE',  ( -6.938893903907228378E-14, -4.618802153517020059, -0.3572655899081733644 ) ) ;
#4736=CARTESIAN_POINT ( 'NONE',  ( 2.678494666091051801, 3.072372537026353267, -0.03421028094653036367 ) ) ;
#4742=CARTESIAN_POINT ( 'NONE',  ( 1.387778780781445676E-14, 4.618802153517020059, 0.000000000000000000 ) ) ;
#4768=FILL_AREA_STYLE ('',( #20902 ) ) ;
#4777=CARTESIAN_POINT ( 'NONE',  ( 0.000000000000000000, 0.000000000000000000, 0.000000000000000000 ) ) ;
#4808=CARTESIAN_POINT ( 'NONE',  ( 2.500000000000000444, 0.000000000000000000, 3.415236843329338967E-15 ) ) ;
#4819=FACE_OUTER_BOUND ( 'NONE', #18298, .T. ) ;
#4830=AXIS2_PLACEMENT_3D ( 'NONE', #1293, #8231, #4913 ) ;
#4873=CARTESIAN_POINT ( 'NONE',  ( 2.339468227445713921, 3.268109542640643905, -5.600000000000002309 ) ) ;
#4881=CARTESIAN_POINT ( 'NONE',  ( 2.000000000000015543, -3.464101615137746837, 0.000000000000000000 ) ) ;
#4913=DIRECTION ( 'NONE',  ( -1.000000000000000000, 0.000000000000000000, 0.000000000000000000 ) ) ;
#4943=CARTESIAN_POINT ( 'NONE',  ( 0.000000000000000000, 0.000000000000000000, 0.000000000000000000 ) ) ;
#4964=CARTESIAN_POINT ( 'NONE',  ( 0.3263565795980740147, -4.430380094434307026, -0.2484800633750381682 ) ) ;
#4991=DIRECTION ( 'NONE',  ( -1.000000000000000000, 0.000000000000000000, 0.000000000000000000 ) ) ;
#4996=CARTESIAN_POINT ( 'NONE',  ( 0.000000000000000000, 0.000000000000000000, 0.000000000000000000 ) ) ;
#5148=DIRECTION ( 'NONE',  ( 1.000000000000000000, 0.000000000000000000, 0.000000000000000000 ) ) ;
#5215=AXIS2_PLACEMENT_3D ( 'NONE', #4777, #10305, #8201 ) ;
#5232=VERTEX_POINT ( 'NONE', #13461 ) ;
#5239=VERTEX_POINT ( 'NONE', #20175 ) ;
#5243=PLANE ( 'NONE',  #15126 ) ;
#5260=CONICAL_SURFACE ( 'NONE', #21025, 4.000000000000000000, 1.047197551196595855 ) ;
#5287=ORIENTED_EDGE ( 'NONE', *, *, #3796, .F. ) ;
#5294=FACE_OUTER_BOUND ( 'NONE', #3994, .T. ) ;
#5306=DIRECTION ( 'NONE',  ( 1.000000000000000000, 0.000000000000000000, 0.000000000000000000 ) ) ;
#5313=ORIENTED_EDGE ( 'NONE', *, *, #2403, .T. ) ;
#5314=ORIENTED_EDGE ( 'NONE', *, *, #13101, .T. ) ;
#5326=CARTESIAN_POINT ( 'NONE',  ( 2.000000000000015543, -3.464101615137746837, 0.000000000000000000 ) ) ;
#5327=FACE_OUTER_BOUND ( 'NONE', #1176, .T. ) ;
#5345=AXIS2_PLACEMENT_3D ( 'NONE', #4742, #10382, #17554 ) ;
#5355=PLANE ( 'NONE',  #1975 ) ;
#5363=( NAMED_UNIT ( * ) PLANE_ANGLE_UNIT ( ) SI_UNIT ( $, .RADIAN. ) );
#5370=ORIENTED_EDGE ( 'NONE', *, *, #11976, .T. ) ;
#5376=ORIENTED_EDGE ( 'NONE', *, *, #21205, .T. ) ;
#5394=DIRECTION ( 'NONE',  ( 1.000000000000000000, 0.000000000000000000, 0.000000000000000000 ) ) ;
#5418=ADVANCED_FACE ( 'NONE', ( #3227, #11910 ), #6406, .F. ) ;
#5435=EDGE_LOOP ( 'NONE', ( #14285, #12987, #7056, #1885, #22393, #1297 ) ) ;
#5453=CARTESIAN_POINT ( 'NONE',  ( 0.000000000000000000, 0.000000000000000000, -5.600000000000000533 ) ) ;
#5505=ADVANCED_FACE ( 'NONE', ( #21344 ), #18872, .F. ) ;
#5584=ORIENTED_EDGE ( 'NONE', *, *, #11690, .T. ) ;
#5593=AXIS2_PLACEMENT_3D ( 'NONE', #4996, #15928, #17584 ) ;
#5609=CYLINDRICAL_SURFACE ( 'NONE', #8613, 2.500000000000002220 ) ;
#5631=CARTESIAN_POINT ( 'NONE',  ( -3.673643420401913939, -2.497823135841291009, -0.2484800633750125221 ) ) ;
#5644=LINE ( 'NONE', #12806, #21420 ) ;
#5684=CARTESIAN_POINT ( 'NONE',  ( 0.000000000000000000, 0.000000000000000000, -5.574599999999999334 ) ) ;
#5829=CARTESIAN_POINT ( 'NONE',  ( 4.000000000000003553, 1.557668341133516599, -0.1596965656957576030 ) ) ;
#5833=EDGE_CURVE ( 'NONE', #9593, #18558, #15711, .T. ) ;
#5865=CARTESIAN_POINT ( 'NONE',  ( -3.344563996438217224, -2.687817229851500400, -0.1586754815285019160 ) ) ;
#5905=CARTESIAN_POINT ( 'NONE',  ( 4.000000000000003553, 2.309401076758480720, -5.600000000000000533 ) ) ;
#5913=AXIS2_PLACEMENT_3D ( 'NONE', #17379, #13638, #20830 ) ;
#5979=CARTESIAN_POINT ( 'NONE',  ( -4.000000000000003553, -2.309401076758532678, -0.3572655899081733644 ) ) ;
#5996=FACE_OUTER_BOUND ( 'NONE', #2375, .T. ) ;
#6009=EDGE_LOOP ( 'NONE', ( #8546, #17361, #10622, #15816, #18818, #21030 ) ) ;
#6021=CARTESIAN_POINT ( 'NONE',  ( -2.000000000000015543, 3.464101615137746837, -5.600000000000000533 ) ) ;
#6047=ADVANCED_FACE ( 'NONE', ( #6115 ), #18688, .T. ) ;
#6061=VERTEX_POINT ( 'NONE', #13054 ) ;
#6068=ORIENTED_EDGE ( 'NONE', *, *, #18922, .T. ) ;
#6079=EDGE_CURVE ( 'NONE', #1148, #16805, #22574, .T. ) ;
#6115=FACE_OUTER_BOUND ( 'NONE', #14514, .T. ) ;
#6135=CARTESIAN_POINT ( 'NONE',  ( -0.6554360035617893265, 4.240386000424037682, -5.441324518471510885 ) ) ;
#6149=EDGE_CURVE ( 'NONE', #19900, #18558, #21296, .T. ) ;
#6187=ORIENTED_EDGE ( 'NONE', *, *, #6794, .F. ) ;
#6215=CARTESIAN_POINT ( 'NONE',  ( -4.000000000000004441, 0.7862748000878184707, -5.565527722372431541 ) ) ;
#6216=ADVANCED_FACE ( 'NONE', ( #17146 ), #17265, .T. ) ;
#6223=ORIENTED_EDGE ( 'NONE', *, *, #13675, .T. ) ;
#6290=CARTESIAN_POINT ( 'NONE',  ( -4.000000000000002665, -0.3902508023145539462, -1.988833360153096802E-15 ) ) ;
#6304=CIRCLE ( 'NONE', #9300, 2.500000000000002220 ) ;
#6332=CIRCLE ( 'NONE', #17589, 4.000000000000000888 ) ;
#6345=DIRECTION ( 'NONE',  ( -1.000000000000000000, 0.000000000000000000, 0.000000000000000000 ) ) ;
#6354=EDGE_CURVE ( 'NONE', #902, #18520, #19384, .T. ) ;
#6406=PLANE ( 'NONE',  #5345 ) ;
#6416=ORIENTED_EDGE ( 'NONE', *, *, #18922, .F. ) ;
#6449=CARTESIAN_POINT ( 'NONE',  ( 0.000000000000000000, 0.000000000000000000, -5.600000000000000533 ) ) ;
#6461=CARTESIAN_POINT ( 'NONE',  ( 0.6543461111163482169, 4.241015250120811153, -0.1391502195351433935 ) ) ;
#6488=AXIS2_PLACEMENT_3D ( 'NONE', #16156, #7241, #9231 ) ;
#6499=VERTEX_POINT ( 'NONE', #6521 ) ;
#6521=CARTESIAN_POINT ( 'NONE',  ( -4.000000000000003553, 0.000000000000000000, 0.000000000000000000 ) ) ;
#6526=SURFACE_STYLE_FILL_AREA ( #4632 ) ;
#6615=CARTESIAN_POINT ( 'NONE',  ( -4.000000000000003553, 0.3904826640788006675, -2.023985227464150660E-15 ) ) ;
#6656=DIRECTION ( 'NONE',  ( -0.8660254037844348218, 0.5000000000000066613, 0.000000000000000000 ) ) ;
#6668=ORIENTED_EDGE ( 'NONE', *, *, #11534, .T. ) ;
#6732=CARTESIAN_POINT ( 'NONE',  ( 0.000000000000000000, 0.000000000000000000, -5.600000000000000533 ) ) ;
#6760=B_SPLINE_CURVE_WITH_KNOTS ( 'NONE', 3,
 ( #23190, #14346, #10584, #17765, #10349, #21193 ),
 .UNSPECIFIED., .F., .F.,
 ( 4, 2, 4 ),
 ( 0.004120275011746847918, 0.005288420935197131814, 0.006456566858647415710 ),
 .UNSPECIFIED. ) ;
#6794=EDGE_CURVE ( 'NONE', #18297, #7463, #14199, .T. ) ;
#6882=AXIS2_PLACEMENT_3D ( 'NONE', #36, #8850, #21217 ) ;
#6992=AXIS2_PLACEMENT_3D ( 'NONE', #19637, #22950, #12690 ) ;
#7056=ORIENTED_EDGE ( 'NONE', *, *, #11264, .T. ) ;
#7097=VERTEX_POINT ( 'NONE', #7417 ) ;
#7137=FACE_OUTER_BOUND ( 'NONE', #19316, .T. ) ;
#7142=SURFACE_SIDE_STYLE ('',( #8771 ) ) ;
#7241=DIRECTION ( 'NONE',  ( 0.000000000000000000, 0.000000000000000000, -1.000000000000000000 ) ) ;
#7255=VERTEX_POINT ( 'NONE', #4808 ) ;
#7259=EDGE_CURVE ( 'NONE', #2262, #1131, #10828, .T. ) ;
#7287=ORIENTED_EDGE ( 'NONE', *, *, #9516, .T. ) ;
#7301=DIRECTION ( 'NONE',  ( 1.000000000000000000, 0.000000000000000000, 0.000000000000000000 ) ) ;
#7309=CARTESIAN_POINT ( 'NONE',  ( -4.000000000000003553, 2.309401076758494487, -0.3572655899081629283 ) ) ;
#7376=VECTOR ( 'NONE', #824, 1000.000000000000000 ) ;
#7405=CARTESIAN_POINT ( 'NONE',  ( 0.000000000000000000, 0.000000000000000000, -5.600000000000000533 ) ) ;
#7417=CARTESIAN_POINT ( 'NONE',  ( 3.999999999999989786, -2.309401076758549998, -5.242734410091827613 ) ) ;
#7421=SHAPE_DEFINITION_REPRESENTATION ( #17764, #9834 ) ;
#7438=AXIS2_PLACEMENT_3D ( 'NONE', #769, #7932, #12255 ) ;
#7463=VERTEX_POINT ( 'NONE', #1 ) ;
#7480=B_SPLINE_CURVE_WITH_KNOTS ( 'NONE', 3,
 ( #7972, #18672, #6215, #20687, #15371, #13384 ),
 .UNSPECIFIED., .F., .F.,
 ( 4, 2, 4 ),
 ( 0.006456566858647396628, 0.007625406818786667311, 0.008794246778925937993 ),
 .UNSPECIFIED. ) ;
#7491=EDGE_CURVE ( 'NONE', #9423, #18520, #9454, .T. ) ;
#7502=LINE ( 'NONE', #22198, #16279 ) ;
#7531=DIRECTION ( 'NONE',  ( -0.5000000000000024425, 0.8660254037844372643, 0.000000000000000000 ) ) ;
#7545=ORIENTED_EDGE ( 'NONE', *, *, #11685, .T. ) ;
#7586=EDGE_CURVE ( 'NONE', #9423, #6499, #715, .T. ) ;
#7591=DIRECTION ( 'NONE',  ( 1.000000000000000000, 0.000000000000000000, 0.000000000000000000 ) ) ;
#7596=AXIS2_PLACEMENT_3D ( 'NONE', #9434, #17170, #2596 ) ;
#7615=AXIS2_PLACEMENT_3D ( 'NONE', #13217, #4268, #11446 ) ;
#7632=CARTESIAN_POINT ( 'NONE',  ( -1.318516776095816523, -3.857556137907097060, -5.599999999999981881 ) ) ;
#7673=EDGE_CURVE ( 'NONE', #7463, #12394, #11840, .T. ) ;
#7775=CARTESIAN_POINT ( 'NONE',  ( 4.000000000000003553, 2.309401076758525573, -5.242734410091827613 ) ) ;
#7923=ADVANCED_FACE ( 'NONE', ( #198 ), #5609, .F. ) ;
#7932=DIRECTION ( 'NONE',  ( -0.000000000000000000, -0.000000000000000000, 1.000000000000000000 ) ) ;
#7948=EDGE_CURVE ( 'NONE', #17189, #3914, #14246, .T. ) ;
#7972=CARTESIAN_POINT ( 'NONE',  ( -4.000000000000003553, 0.000000000000000000, -5.600000000000000533 ) ) ;
#7974=ORIENTED_EDGE ( 'NONE', *, *, #3079, .F. ) ;
#7991=CARTESIAN_POINT ( 'NONE',  ( -2.060000000000002718, 2.522772406243550895E-16, -0.3080913168122707546 ) ) ;
#8022=DIRECTION ( 'NONE',  ( 0.000000000000000000, -0.000000000000000000, 1.000000000000000000 ) ) ;
#8032=CONICAL_SURFACE ( 'NONE', #517, 4.000000000000000000, 1.047197551196595855 ) ;
#8042=CARTESIAN_POINT ( 'NONE',  ( 3.344563996438205677, 2.687817229851463985, -0.1586754815284830145 ) ) ;
#8053=ORIENTED_EDGE ( 'NONE', *, *, #6079, .F. ) ;
#8069=DIRECTION ( 'NONE',  ( 0.000000000000000000, 0.000000000000000000, -1.000000000000000000 ) ) ;
#8084=ORIENTED_EDGE ( 'NONE', *, *, #11976, .F. ) ;
#8116=ORIENTED_EDGE ( 'NONE', *, *, #21205, .F. ) ;
#8182=CARTESIAN_POINT ( 'NONE',  ( 2.099999999999999645, 0.000000000000000000, -0.2800830152838856835 ) ) ;
#8201=DIRECTION ( 'NONE',  ( -1.000000000000000000, 0.000000000000000000, 0.000000000000000000 ) ) ;
#8231=DIRECTION ( 'NONE',  ( 0.000000000000000000, -0.000000000000000000, 1.000000000000000000 ) ) ;
#8269=ORIENTED_EDGE ( 'NONE', *, *, #9645, .F. ) ;
#8272=EDGE_CURVE ( 'NONE', #6061, #20542, #7480, .T. ) ;
#8277=DIRECTION ( 'NONE',  ( -0.000000000000000000, -0.000000000000000000, 1.000000000000000000 ) ) ;
#8296=ORIENTED_EDGE ( 'NONE', *, *, #679, .F. ) ;
#8429=CYLINDRICAL_SURFACE ( 'NONE', #19465, 2.099999999999999645 ) ;
#8449=CARTESIAN_POINT ( 'NONE',  ( -0.6543461111163908495, -4.241015250120827140, -0.1391502195351569937 ) ) ;
#8483=CARTESIAN_POINT ( 'NONE',  ( -3.345653888883665772, 2.687187980154696731, -5.460849780464863024 ) ) ;
#8533=CARTESIAN_POINT ( 'NONE',  ( 2.000000000000029310, 3.464101615137740175, -5.600000000000000533 ) ) ;
#8541=LINE ( 'NONE', #916, #9361 ) ;
#8546=ORIENTED_EDGE ( 'NONE', *, *, #6354, .T. ) ;
#8571=CARTESIAN_POINT ( 'NONE',  ( 0.000000000000000000, 0.000000000000000000, 3.469446951953614189E-15 ) ) ;
#8572=DIRECTION ( 'NONE',  ( 0.000000000000000000, 0.000000000000000000, 1.000000000000000000 ) ) ;
#8613=AXIS2_PLACEMENT_3D ( 'NONE', #419, #3941, #7591 ) ;
#8643=CARTESIAN_POINT ( 'NONE',  ( 1.387778780781445676E-14, 4.618802153517020059, -5.600000000000000533 ) ) ;
#8677=DIRECTION ( 'NONE',  ( -0.000000000000000000, -0.000000000000000000, 1.000000000000000000 ) ) ;
#8682=EDGE_CURVE ( 'NONE', #6499, #18441, #18674, .T. ) ;
#8715=ADVANCED_FACE ( 'NONE', ( #15656 ), #2370, .T. ) ;
#8765=EDGE_CURVE ( 'NONE', #16716, #4023, #21554, .T. ) ;
#8771=SURFACE_STYLE_FILL_AREA ( #4768 ) ;
#8821=ORIENTED_EDGE ( 'NONE', *, *, #15985, .T. ) ;
#8850=DIRECTION ( 'NONE',  ( 0.000000000000000000, -0.000000000000000000, 1.000000000000000000 ) ) ;
#9020=B_SPLINE_CURVE_WITH_KNOTS ( 'NONE', 3,
 ( #13568, #17547, #4736, #8042, #4505, #11672 ),
 .UNSPECIFIED., .F., .F.,
 ( 4, 2, 4 ),
 ( 0.002336974151641583747, 0.003500975885716454093, 0.004664977619791324873 ),
 .UNSPECIFIED. ) ;
#9023=ORIENTED_EDGE ( 'NONE', *, *, #23227, .T. ) ;
#9146=CIRCLE ( 'NONE', #14782, 2.099999999999999645 ) ;
#9231=DIRECTION ( 'NONE',  ( -1.000000000000000000, 0.000000000000000000, 0.000000000000000000 ) ) ;
#9286=CARTESIAN_POINT ( 'NONE',  ( 0.000000000000000000, 0.000000000000000000, -5.600000000000000533 ) ) ;
#9300=AXIS2_PLACEMENT_3D ( 'NONE', #4320, #9408, #16782 ) ;
#9313=PLANE ( 'NONE',  #867 ) ;
#9320=AXIS2_PLACEMENT_3D ( 'NONE', #14320, #8677, #5394 ) ;
#9361=VECTOR ( 'NONE', #13492, 1000.000000000000000 ) ;
#9367=EDGE_LOOP ( 'NONE', ( #20359, #12261, #16827 ) ) ;
#9408=DIRECTION ( 'NONE',  ( -0.000000000000000000, -0.000000000000000000, 1.000000000000000000 ) ) ;
#9423=VERTEX_POINT ( 'NONE', #11493 ) ;
#9434=CARTESIAN_POINT ( 'NONE',  ( 0.000000000000000000, 0.000000000000000000, -0.2800830152838856835 ) ) ;
#9454=B_SPLINE_CURVE_WITH_KNOTS ( 'NONE', 3,
 ( #2205, #13260, #20443, #5865, #5631, #5979 ),
 .UNSPECIFIED., .F., .F.,
 ( 4, 2, 4 ),
 ( 0.002336974151641598059, 0.003500975885716476645, 0.004664977619791355230 ),
 .UNSPECIFIED. ) ;
#9516=EDGE_CURVE ( 'NONE', #1131, #2262, #11735, .T. ) ;
#9593=VERTEX_POINT ( 'NONE', #17609 ) ;
#9624=CARTESIAN_POINT ( 'NONE',  ( -4.000000000000003553, -0.3902508023145539462, -5.599999999999998757 ) ) ;
#9625=EDGE_LOOP ( 'NONE', ( #12642, #17294, #16894, #1545, #21924, #21079 ) ) ;
#9645=EDGE_CURVE ( 'NONE', #14161, #3914, #3801, .T. ) ;
#9658=CARTESIAN_POINT ( 'NONE',  ( 1.387778780781445676E-14, 4.618802153517020059, -5.242734410091827613 ) ) ;
#9660=CARTESIAN_POINT ( 'NONE',  ( 0.000000000000000000, 0.000000000000000000, -5.600000000000000533 ) ) ;
#9711=VERTEX_POINT ( 'NONE', #14889 ) ;
#9752=DIRECTION ( 'NONE',  ( 0.000000000000000000, 0.000000000000000000, 1.000000000000000000 ) ) ;
#9799=ORIENTED_EDGE ( 'NONE', *, *, #21470, .F. ) ;
#9802=B_SPLINE_CURVE_WITH_KNOTS ( 'NONE', 3,
 ( #2955, #13661, #4478, #17524, #11647, #15296 ),
 .UNSPECIFIED., .F., .F.,
 ( 4, 2, 4 ),
 ( 0.002336974151641598059, 0.003500975885716476645, 0.004664977619791355230 ),
 .UNSPECIFIED. ) ;
#9803=DIRECTION ( 'NONE',  ( -0.000000000000000000, -0.000000000000000000, 1.000000000000000000 ) ) ;
#9834=SHAPE_REPRESENTATION ( 'hex nut gradec_bsi_BS EN 24034 - M5 - N', ( #22115 ), #2988 ) ;
#9890=DIRECTION ( 'NONE',  ( 0.000000000000000000, 0.000000000000000000, 1.000000000000000000 ) ) ;
#9930=CARTESIAN_POINT ( 'NONE',  ( 2.681483223904248980, -3.070647092368468112, -5.599999999999979217 ) ) ;
#9942=( NAMED_UNIT ( * ) SI_UNIT ( $, .STERADIAN. ) SOLID_ANGLE_UNIT ( ) );
#9943=ORIENTED_EDGE ( 'NONE', *, *, #912, .F. ) ;
#9983=DIRECTION ( 'NONE',  ( -1.000000000000000000, 0.000000000000000000, 0.000000000000000000 ) ) ;
#10001=ORIENTED_EDGE ( 'NONE', *, *, #2900, .T. ) ;
#10021=DIRECTION ( 'NONE',  ( -1.000000000000000000, 0.000000000000000000, 0.000000000000000000 ) ) ;
#10045=VECTOR ( 'NONE', #13866, 1000.000000000000000 ) ;
#10106=ADVANCED_FACE ( 'NONE', ( #15581, #21122 ), #5355, .T. ) ;
#10117=ADVANCED_FACE ( 'NONE', ( #14294 ), #5243, .T. ) ;
#10191=MECHANICAL_DESIGN_GEOMETRIC_PRESENTATION_REPRESENTATION('',(#13579),#11682);
#10270=CARTESIAN_POINT ( 'NONE',  ( -4.000000000000003553, 0.000000000000000000, 0.000000000000000000 ) ) ;
#10305=DIRECTION ( 'NONE',  ( -0.000000000000000000, 0.000000000000000000, -1.000000000000000000 ) ) ;
#10311=ADVANCED_BREP_SHAPE_REPRESENTATION ( '', ( #20673, #22115 ), #2988 ) ;
#10349=CARTESIAN_POINT ( 'NONE',  ( 4.000000000000003553, -0.3902508023145569993, -1.999844788467403101E-15 ) ) ;
#10369=CARTESIAN_POINT ( 'NONE',  ( -4.000000000000002665, 1.557668341133494838, -0.1596965656957533841 ) ) ;
#10371=EDGE_CURVE ( 'NONE', #12394, #1148, #9146, .T. ) ;
#10382=DIRECTION ( 'NONE',  ( 0.000000000000000000, 0.000000000000000000, -1.000000000000000000 ) ) ;
#10385=ADVANCED_FACE ( 'NONE', ( #4148 ), #16263, .F. ) ;
#10409=CARTESIAN_POINT ( 'NONE',  ( -3.345653888883676430, 2.687187980154690958, -0.1391502195351397297 ) ) ;
#10418=( NAMED_UNIT ( * ) SI_UNIT ( $, .STERADIAN. ) SOLID_ANGLE_UNIT ( ) );
#10514=ADVANCED_FACE ( 'NONE', ( #5294 ), #2387, .T. ) ;
#10551=CARTESIAN_POINT ( 'NONE',  ( 3.345653888883671989, -2.687187980154742473, -0.1391502195351571880 ) ) ;
#10584=CARTESIAN_POINT ( 'NONE',  ( 4.000000000000004441, -1.549102112939114484, -0.1578953385959453726 ) ) ;
#10609=DIRECTION ( 'NONE',  ( 0.000000000000000000, -0.000000000000000000, 1.000000000000000000 ) ) ;
#10622=ORIENTED_EDGE ( 'NONE', *, *, #8682, .T. ) ;
#10637=CARTESIAN_POINT ( 'NONE',  ( -4.000000000000003553, 2.309401076758494487, -0.3572655899081629283 ) ) ;
#10733=DIRECTION ( 'NONE',  ( 0.000000000000000000, 0.000000000000000000, -1.000000000000000000 ) ) ;
#10738=LINE ( 'NONE', #12495, #12309 ) ;
#10756=CARTESIAN_POINT ( 'NONE',  ( 3.999999999999989786, -2.309401076758549998, -5.242734410091827613 ) ) ;
#10763=B_SPLINE_CURVE_WITH_KNOTS ( 'NONE', 3,
 ( #20332, #4192, #2444, #14677, #9624, #16774 ),
 .UNSPECIFIED., .F., .F.,
 ( 4, 2, 4 ),
 ( 0.004120275011746843581, 0.005288420935197119671, 0.006456566858647396628 ),
 .UNSPECIFIED. ) ;
#10804=EDGE_LOOP ( 'NONE', ( #5314, #18997, #7545, #3693, #1721, #7974 ) ) ;
#10820=DIRECTION ( 'NONE',  ( -0.000000000000000000, 0.000000000000000000, -1.000000000000000000 ) ) ;
#10828=CIRCLE ( 'NONE', #4830, 2.500000000000002220 ) ;
#10834=ORIENTED_EDGE ( 'NONE', *, *, #7586, .F. ) ;
#10866=CARTESIAN_POINT ( 'NONE',  ( 4.000000000000004441, 0.7862748000878158061, -0.03447227762756879116 ) ) ;
#10909=EDGE_LOOP ( 'NONE', ( #22913, #2412, #8269 ) ) ;
#10970=ORIENTED_EDGE ( 'NONE', *, *, #2180, .F. ) ;
#11014=AXIS2_PLACEMENT_3D ( 'NONE', #17669, #10609, #12962 ) ;
#11039=DIRECTION ( 'NONE',  ( -0.000000000000000000, -0.000000000000000000, 1.000000000000000000 ) ) ;
#11049=AXIS2_PLACEMENT_3D ( 'NONE', #5453, #3446, #3343 ) ;
#11193=DIRECTION ( 'NONE',  ( 1.000000000000000000, 0.000000000000000000, 0.000000000000000000 ) ) ;
#11208=AXIS2_PLACEMENT_3D ( 'NONE', #4593, #11776, #10021 ) ;
#11217=CARTESIAN_POINT ( 'NONE',  ( 4.000000000000003553, 2.309401076758525573, -0.3572655899081733644 ) ) ;
#11237=EDGE_LOOP ( 'NONE', ( #22122, #17896, #9023 ) ) ;
#11264=EDGE_CURVE ( 'NONE', #7097, #1072, #17461, .T. ) ;
#11431=ORIENTED_EDGE ( 'NONE', *, *, #7673, .T. ) ;
#11446=DIRECTION ( 'NONE',  ( -1.000000000000000000, 0.000000000000000000, 0.000000000000000000 ) ) ;
#11493=CARTESIAN_POINT ( 'NONE',  ( -2.000000000000015543, -3.464101615137743728, 0.000000000000000000 ) ) ;
#11534=EDGE_CURVE ( 'NONE', #7463, #18297, #14746, .T. ) ;
#11623=CARTESIAN_POINT ( 'NONE',  ( -6.938893903907228378E-14, -4.618802153517020059, -0.3572655899081733644 ) ) ;
#11647=CARTESIAN_POINT ( 'NONE',  ( -3.673643420401913939, -2.497823135841291009, -5.351519936624987928 ) ) ;
#11652=DIRECTION ( 'NONE',  ( -0.000000000000000000, -0.000000000000000000, 1.000000000000000000 ) ) ;
#11672=CARTESIAN_POINT ( 'NONE',  ( 4.000000000000003553, 2.309401076758525573, -0.3572655899081733644 ) ) ;
#11682=( GEOMETRIC_REPRESENTATION_CONTEXT ( 3 ) GLOBAL_UNCERTAINTY_ASSIGNED_CONTEXT ( ( #15192 ) ) GLOBAL_UNIT_ASSIGNED_CONTEXT ( ( #3135, #5363, #10418 ) ) REPRESENTATION_CONTEXT ( 'NONE', 'WORKASPACE' ) );
#11685=EDGE_CURVE ( 'NONE', #3914, #20222, #14384, .T. ) ;
#11690=EDGE_CURVE ( 'NONE', #18297, #1148, #12142, .T. ) ;
#11706=EDGE_CURVE ( 'NONE', #5239, #13382, #21175, .T. ) ;
#11709=FACE_OUTER_BOUND ( 'NONE', #12976, .T. ) ;
#11716=VECTOR ( 'NONE', #9752, 1000.000000000000000 ) ;
#11728=DIRECTION ( 'NONE',  ( -1.000000000000000000, 0.000000000000000000, 0.000000000000000000 ) ) ;
#11735=CIRCLE ( 'NONE', #2347, 2.500000000000002220 ) ;
#11776=DIRECTION ( 'NONE',  ( 0.000000000000000000, -0.000000000000000000, 1.000000000000000000 ) ) ;
#11780=ORIENTED_EDGE ( 'NONE', *, *, #3796, .T. ) ;
#11803=CARTESIAN_POINT ( 'NONE',  ( -4.000000000000003553, -2.309401076758532678, -0.3572655899081733644 ) ) ;
#11812=SURFACE_STYLE_USAGE ( .BOTH. , #15095 ) ;
#11840=LINE ( 'NONE', #1265, #3336 ) ;
#11854=DIRECTION ( 'NONE',  ( -0.000000000000000000, 0.000000000000000000, -1.000000000000000000 ) ) ;
#11910=FACE_OUTER_BOUND ( 'NONE', #21885, .T. ) ;
#11923=ORIENTED_EDGE ( 'NONE', *, *, #679, .T. ) ;
#11976=EDGE_CURVE ( 'NONE', #20222, #9423, #3676, .T. ) ;
#12009=ORIENTED_EDGE ( 'NONE', *, *, #22875, .T. ) ;
#12023=CARTESIAN_POINT ( 'NONE',  ( -4.000000000000004441, -1.549102112939104492, -0.1578953385959430966 ) ) ;
#12108=CARTESIAN_POINT ( 'NONE',  ( -4.000000000000003553, 2.309401076758532678, -5.242734410091827613 ) ) ;
#12142=LINE ( 'NONE', #19328, #1261 ) ;
#12249=DIRECTION ( 'NONE',  ( 0.000000000000000000, 0.000000000000000000, 1.000000000000000000 ) ) ;
#12255=DIRECTION ( 'NONE',  ( 1.000000000000000000, 0.000000000000000000, 0.000000000000000000 ) ) ;
#12261=ORIENTED_EDGE ( 'NONE', *, *, #19638, .T. ) ;
#12274=CARTESIAN_POINT ( 'NONE',  ( 0.000000000000000000, -4.618802153517061804, -5.600000000000000533 ) ) ;
#12301=ORIENTED_EDGE ( 'NONE', *, *, #14747, .T. ) ;
#12309=VECTOR ( 'NONE', #15671, 1000.000000000000000 ) ;
#12394=VERTEX_POINT ( 'NONE', #8182 ) ;
#12417=ORIENTED_EDGE ( 'NONE', *, *, #13406, .F. ) ;
#12423=VERTEX_POINT ( 'NONE', #2881 ) ;
#12485=CARTESIAN_POINT ( 'NONE',  ( -6.938893903907228378E-14, -4.618802153517020059, -0.3572655899081733644 ) ) ;
#12495=CARTESIAN_POINT ( 'NONE',  ( -2.500000000000002220, 0.000000000000000000, -5.574599999999999334 ) ) ;
#12576=FACE_OUTER_BOUND ( 'NONE', #21442, .T. ) ;
#12642=ORIENTED_EDGE ( 'NONE', *, *, #23227, .F. ) ;
#12671=DIRECTION ( 'NONE',  ( 0.000000000000000000, 0.000000000000000000, 1.000000000000000000 ) ) ;
#12690=DIRECTION ( 'NONE',  ( 1.000000000000000000, 0.000000000000000000, 0.000000000000000000 ) ) ;
#12717=ORIENTED_EDGE ( 'NONE', *, *, #7491, .T. ) ;
#12754=EDGE_CURVE ( 'NONE', #17189, #9711, #18793, .T. ) ;
#12806=CARTESIAN_POINT ( 'NONE',  ( -2.500000000000002220, 3.061616997868386099E-16, -25.03750572909317285 ) ) ;
#12849=CIRCLE ( 'NONE', #7596, 2.099999999999999645 ) ;
#12853=EDGE_LOOP ( 'NONE', ( #13763, #3178, #14432 ) ) ;
#12857=ORIENTED_EDGE ( 'NONE', *, *, #16843, .F. ) ;
#12929=DIRECTION ( 'NONE',  ( 0.000000000000000000, 0.000000000000000000, 1.000000000000000000 ) ) ;
#12936=CLOSED_SHELL ( 'NONE', ( #7923, #2723, #4086, #2072, #2637, #6047, #3904, #20783, #10117, #17106, #6216, #5418, #10106, #18042, #13405, #10514, #2339, #18279, #8715, #13722, #17552, #20401, #4547, #16605, #13281, #10385, #5505, #1488 ) ) ;
#12962=DIRECTION ( 'NONE',  ( -1.000000000000000000, -1.776356839400250465E-15, 0.000000000000000000 ) ) ;
#12976=EDGE_LOOP ( 'NONE', ( #8821, #1881, #858, #19114, #21834, #21703 ) ) ;
#12980=B_SPLINE_CURVE_WITH_KNOTS ( 'NONE', 3,
 ( #8533, #4873, #17465, #23004, #20896, #4651 ),
 .UNSPECIFIED., .F., .F.,
 ( 4, 2, 4 ),
 ( 0.002336974151641583314, 0.003500975885716454093, 0.004664977619791324873 ),
 .UNSPECIFIED. ) ;
#12987=ORIENTED_EDGE ( 'NONE', *, *, #13101, .F. ) ;
#13008=EDGE_LOOP ( 'NONE', ( #175, #5376, #10970, #17298 ) ) ;
#13054=CARTESIAN_POINT ( 'NONE',  ( -4.000000000000003553, 0.000000000000000000, -5.600000000000000533 ) ) ;
#13086=ORIENTED_EDGE ( 'NONE', *, *, #18406, .F. ) ;
#13101=EDGE_CURVE ( 'NONE', #7097, #14161, #604, .T. ) ;
#13217=CARTESIAN_POINT ( 'NONE',  ( 0.000000000000000000, 0.000000000000000000, -5.294516984716112873 ) ) ;
#13224=FACE_OUTER_BOUND ( 'NONE', #143, .T. ) ;
#13260=CARTESIAN_POINT ( 'NONE',  ( -2.339468227445725468, -3.268109542640679432, -1.836070968115783499E-14 ) ) ;
#13281=ADVANCED_FACE ( 'NONE', ( #4819 ), #1491, .T. ) ;
#13284=LINE ( 'NONE', #20234, #13936 ) ;
#13289=CARTESIAN_POINT ( 'NONE',  ( 1.387778780781445676E-14, 4.618802153517020059, -5.600000000000000533 ) ) ;
#13315=CARTESIAN_POINT ( 'NONE',  ( -1.321505333908965962, 3.855830693249139962, -0.03421028094653124491 ) ) ;
#13347=CARTESIAN_POINT ( 'NONE',  ( -4.000000000000003553, -1.933795701539610556, -0.2488376576623001213 ) ) ;
#13353=SHAPE_REPRESENTATION_RELATIONSHIP ( 'NONE' , 'NONE' ,  #9834, #10311 ) ;
#13368=DIRECTION ( 'NONE',  ( 1.000000000000000000, 0.000000000000000000, 0.000000000000000000 ) ) ;
#13382=VERTEX_POINT ( 'NONE', #21426 ) ;
#13384=CARTESIAN_POINT ( 'NONE',  ( -4.000000000000003553, 2.309401076758532678, -5.242734410091827613 ) ) ;
#13401=CONICAL_SURFACE ( 'NONE', #16037, 4.000000000000000000, 1.047197551196595855 ) ;
#13405=ADVANCED_FACE ( 'NONE', ( #12576 ), #5260, .T. ) ;
#13406=EDGE_CURVE ( 'NONE', #2262, #20512, #5644, .T. ) ;
#13418=VECTOR ( 'NONE', #8572, 1000.000000000000000 ) ;
#13461=CARTESIAN_POINT ( 'NONE',  ( 2.500000000000002220, 3.061616997868386099E-16, -5.574599999999999334 ) ) ;
#13468=PRESENTATION_STYLE_ASSIGNMENT (( #11812 ) ) ;
#13469=ORIENTED_EDGE ( 'NONE', *, *, #6354, .F. ) ;
#13492=DIRECTION ( 'NONE',  ( 0.8191520442889886899, 0.000000000000000000, 0.5735764363510506003 ) ) ;
#13500=( GEOMETRIC_REPRESENTATION_CONTEXT ( 3 ) GLOBAL_UNCERTAINTY_ASSIGNED_CONTEXT ( ( #3940 ) ) GLOBAL_UNIT_ASSIGNED_CONTEXT ( ( #22291, #17214, #17325 ) ) REPRESENTATION_CONTEXT ( 'NONE', 'WORKASPACE' ) );
#13506=CARTESIAN_POINT ( 'NONE',  ( -1.318516776095816523, -3.857556137907097060, -1.903157303500181160E-14 ) ) ;
#13559=ORIENTED_EDGE ( 'NONE', *, *, #1080, .T. ) ;
#13562=CARTESIAN_POINT ( 'NONE',  ( -4.000000000000002665, 1.935983797701051667, -0.2494693066162282091 ) ) ;
#13568=CARTESIAN_POINT ( 'NONE',  ( 2.000000000000029310, 3.464101615137740175, 0.000000000000000000 ) ) ;
#13579=STYLED_ITEM ( 'NONE', ( #15933 ), #20673 ) ;
#13586=( NAMED_UNIT ( * ) PLANE_ANGLE_UNIT ( ) SI_UNIT ( $, .RADIAN. ) );
#13638=DIRECTION ( 'NONE',  ( -1.000000000000000000, 0.000000000000000000, 0.000000000000000000 ) ) ;
#13661=CARTESIAN_POINT ( 'NONE',  ( -2.339468227445725024, -3.268109542640679432, -5.599999999999982769 ) ) ;
#13675=EDGE_CURVE ( 'NONE', #18441, #9593, #738, .T. ) ;
#13719=FACE_OUTER_BOUND ( 'NONE', #13008, .T. ) ;
#13722=ADVANCED_FACE ( 'NONE', ( #18283 ), #4124, .T. ) ;
#13763=ORIENTED_EDGE ( 'NONE', *, *, #7586, .T. ) ;
#13794=CYLINDRICAL_SURFACE ( 'NONE', #2846, 2.500000000000002220 ) ;
#13866=DIRECTION ( 'NONE',  ( -0.8191520442889886899, 1.003171929053520926E-16, 0.5735764363510506003 ) ) ;
#13887=CARTESIAN_POINT ( 'NONE',  ( 4.000000000000003553, 0.000000000000000000, 0.000000000000000000 ) ) ;
#13894=AXIS2_PLACEMENT_3D ( 'NONE', #3699, #21597, #14516 ) ;
#13936=VECTOR ( 'NONE', #20463, 1000.000000000000000 ) ;
#13963=CARTESIAN_POINT ( 'NONE',  ( 0.000000000000000000, 0.000000000000000000, -5.600000000000000533 ) ) ;
#14064=DIRECTION ( 'NONE',  ( 0.000000000000000000, 0.000000000000000000, -1.000000000000000000 ) ) ;
#14131=EDGE_LOOP ( 'NONE', ( #13559, #8084, #16143 ) ) ;
#14139=DIRECTION ( 'NONE',  ( -0.000000000000000000, -0.000000000000000000, 1.000000000000000000 ) ) ;
#14147=DIRECTION ( 'NONE',  ( -0.000000000000000000, 0.000000000000000000, -1.000000000000000000 ) ) ;
#14161=VERTEX_POINT ( 'NONE', #1786 ) ;
#14174=DIRECTION ( 'NONE',  ( 0.5000000000000025535, -0.8660254037844371533, 0.000000000000000000 ) ) ;
#14199=CIRCLE ( 'NONE', #14935, 2.099999999999999645 ) ;
#14204=CONICAL_SURFACE ( 'NONE', #22464, 2.060000000000002718, 0.9599310885968758145 ) ;
#14229=ORIENTED_EDGE ( 'NONE', *, *, #12754, .T. ) ;
#14246=CIRCLE ( 'NONE', #19123, 3.999999999999999112 ) ;
#14269=CARTESIAN_POINT ( 'NONE',  ( 1.660531772554329821, -3.660093687634886628, -2.145195642216240408E-14 ) ) ;
#14285=ORIENTED_EDGE ( 'NONE', *, *, #17277, .F. ) ;
#14294=FACE_OUTER_BOUND ( 'NONE', #10804, .T. ) ;
#14316=CARTESIAN_POINT ( 'NONE',  ( 3.999999999999989786, -2.309401076758549998, -0.3572655899081733644 ) ) ;
#14320=CARTESIAN_POINT ( 'NONE',  ( 0.000000000000000000, 0.000000000000000000, 0.000000000000000000 ) ) ;
#14336=APPLICATION_CONTEXT ( 'automotive_design' ) ;
#14346=CARTESIAN_POINT ( 'NONE',  ( 4.000000000000003553, -1.933795701539624101, -0.2488376576623034797 ) ) ;
#14350=CARTESIAN_POINT ( 'NONE',  ( 0.000000000000000000, 0.000000000000000000, 0.000000000000000000 ) ) ;
#14384=B_SPLINE_CURVE_WITH_KNOTS ( 'NONE', 3,
 ( #5326, #14269, #23107, #21098, #4964, #12485 ),
 .UNSPECIFIED., .F., .F.,
 ( 4, 2, 4 ),
 ( 0.002336974151641521731, 0.003500975885716451057, 0.004664977619791380384 ),
 .UNSPECIFIED. ) ;
#14388=EDGE_CURVE ( 'NONE', #20542, #18441, #727, .T. ) ;
#14432=ORIENTED_EDGE ( 'NONE', *, *, #7491, .F. ) ;
#14508=EDGE_LOOP ( 'NONE', ( #14731, #19166, #16797 ) ) ;
#14514=EDGE_LOOP ( 'NONE', ( #15241, #6223, #22995, #19642, #3802, #13086 ) ) ;
#14516=DIRECTION ( 'NONE',  ( -1.000000000000000000, 0.000000000000000000, 0.000000000000000000 ) ) ;
#14569=CARTESIAN_POINT ( 'NONE',  ( -2.000000000000015543, -3.464101615137743728, -5.600000000000000533 ) ) ;
#14591=AXIS2_PLACEMENT_3D ( 'NONE', #13963, #16184, #5148 ) ;
#14595=AXIS2_PLACEMENT_3D ( 'NONE', #13289, #7531, #14693 ) ;
#14614=DIRECTION ( 'NONE',  ( -1.000000000000000000, 0.000000000000000000, 0.000000000000000000 ) ) ;
#14626=EDGE_LOOP ( 'NONE', ( #3819, #1406, #11431, #15681 ) ) ;
#14677=CARTESIAN_POINT ( 'NONE',  ( -4.000000000000003553, -0.7779732554280798240, -5.566455648918319454 ) ) ;
#14693=DIRECTION ( 'NONE',  ( -0.8660254037844372643, -0.5000000000000024425, 0.000000000000000000 ) ) ;
#14731=ORIENTED_EDGE ( 'NONE', *, *, #4503, .T. ) ;
#14746=CIRCLE ( 'NONE', #7615, 2.099999999999999645 ) ;
#14747=EDGE_CURVE ( 'NONE', #21589, #20222, #13284, .T. ) ;
#14764=EDGE_LOOP ( 'NONE', ( #12417, #22330, #20623, #11923 ) ) ;
#14777=CIRCLE ( 'NONE', #4631, 2.500000000000000444 ) ;
#14782=AXIS2_PLACEMENT_3D ( 'NONE', #4376, #17518, #20950 ) ;
#14787=CARTESIAN_POINT ( 'NONE',  ( -4.000000000000003553, 2.309401076758532678, -5.242734410091827613 ) ) ;
#14802=CARTESIAN_POINT ( 'NONE',  ( -4.000000000000003553, -2.309401076758532678, -5.242734410091827613 ) ) ;
#14823=B_SPLINE_CURVE_WITH_KNOTS ( 'NONE', 3,
 ( #6021, #612, #21902, #6135, #4230, #9658 ),
 .UNSPECIFIED., .F., .F.,
 ( 4, 2, 4 ),
 ( 0.002336974151641528670, 0.003500975885716446721, 0.004664977619791364771 ),
 .UNSPECIFIED. ) ;
#14835=CARTESIAN_POINT ( 'NONE',  ( 1.318516776095790322, 3.857556137907070859, -5.600000000000003197 ) ) ;
#14845=CARTESIAN_POINT ( 'NONE',  ( 1.321505333908973290, -3.855830693249184815, -5.565789719053443996 ) ) ;
#14847=DIRECTION ( 'NONE',  ( -1.000000000000000000, 0.000000000000000000, 0.000000000000000000 ) ) ;
#14863=DIRECTION ( 'NONE',  ( -0.000000000000000000, -0.000000000000000000, 1.000000000000000000 ) ) ;
#14889=CARTESIAN_POINT ( 'NONE',  ( 4.000000000000003553, 2.309401076758525573, -0.3572655899081733644 ) ) ;
#14913=CARTESIAN_POINT ( 'NONE',  ( -0.6543461111163909605, -4.241015250120827140, -5.460849780464843484 ) ) ;
#14935=AXIS2_PLACEMENT_3D ( 'NONE', #20145, #11652, #14847 ) ;
#14945=CARTESIAN_POINT ( 'NONE',  ( -4.000000000000003553, -2.309401076758525573, -5.600000000000000533 ) ) ;
#14986=CARTESIAN_POINT ( 'NONE',  ( 0.000000000000000000, 0.000000000000000000, -0.3080913168122707546 ) ) ;
#15057=CARTESIAN_POINT ( 'NONE',  ( -2.000000000000015543, 3.464101615137746837, 0.000000000000000000 ) ) ;
#15095=SURFACE_SIDE_STYLE ('',( #6526 ) ) ;
#15125=B_SPLINE_CURVE_WITH_KNOTS ( 'NONE', 3,
 ( #12108, #8483, #22839, #18833 ),
 .UNSPECIFIED., .F., .F.,
 ( 4, 4 ),
 ( 2.380737581730922818E-07, 0.002336974151641528670 ),
 .UNSPECIFIED. ) ;
#15126=AXIS2_PLACEMENT_3D ( 'NONE', #12274, #14174, #3006 ) ;
#15142=ORIENTED_EDGE ( 'NONE', *, *, #23203, .T. ) ;
#15152=CYLINDRICAL_SURFACE ( 'NONE', #20593, 2.099999999999999645 ) ;
#15192=UNCERTAINTY_MEASURE_WITH_UNIT (LENGTH_MEASURE( 1.000000000000000082E-05 ), #3135, 'distance_accuracy_value', 'NONE');
#15228=CARTESIAN_POINT ( 'NONE',  ( 0.000000000000000000, 0.000000000000000000, -5.574599999999999334 ) ) ;
#15241=ORIENTED_EDGE ( 'NONE', *, *, #14388, .T. ) ;
#15296=CARTESIAN_POINT ( 'NONE',  ( -4.000000000000003553, -2.309401076758532678, -5.242734410091827613 ) ) ;
#15342=B_SPLINE_CURVE_WITH_KNOTS ( 'NONE', 3,
 ( #11803, #13347, #12023, #18990, #6290, #10270 ),
 .UNSPECIFIED., .F., .F.,
 ( 4, 2, 4 ),
 ( 0.004120275011746843581, 0.005288420935197119671, 0.006456566858647396628 ),
 .UNSPECIFIED. ) ;
#15367=ORIENTED_EDGE ( 'NONE', *, *, #8272, .T. ) ;
#15371=CARTESIAN_POINT ( 'NONE',  ( -4.000000000000003553, 1.935983797701083642, -5.350530693383765524 ) ) ;
#15374=ORIENTED_EDGE ( 'NONE', *, *, #15397, .F. ) ;
#15397=EDGE_CURVE ( 'NONE', #1072, #12423, #22266, .T. ) ;
#15480=EDGE_CURVE ( 'NONE', #1148, #12394, #12849, .T. ) ;
#15529=AXIS2_PLACEMENT_3D ( 'NONE', #1755, #16207, #7301 ) ;
#15553=FACE_OUTER_BOUND ( 'NONE', #14764, .T. ) ;
#15581=FACE_BOUND ( 'NONE', #16836, .T. ) ;
#15591=CARTESIAN_POINT ( 'NONE',  ( 4.000000000000003553, 2.309401076758480720, -5.600000000000000533 ) ) ;
#15635=DIRECTION ( 'NONE',  ( -1.000000000000000000, 0.000000000000000000, 0.000000000000000000 ) ) ;
#15656=FACE_OUTER_BOUND ( 'NONE', #11237, .T. ) ;
#15671=DIRECTION ( 'NONE',  ( -0.8191520442889927978, 0.000000000000000000, -0.5735764363510447161 ) ) ;
#15681=ORIENTED_EDGE ( 'NONE', *, *, #15480, .F. ) ;
#15692=EDGE_CURVE ( 'NONE', #902, #6061, #10763, .T. ) ;
#15703=CIRCLE ( 'NONE', #9320, 4.000000000000000000 ) ;
#15711=CIRCLE ( 'NONE', #22865, 3.999999999999999112 ) ;
#15754=DIRECTION ( 'NONE',  ( 0.000000000000000000, 0.000000000000000000, -1.000000000000000000 ) ) ;
#15793=ORIENTED_EDGE ( 'NONE', *, *, #5833, .F. ) ;
#15800=DIRECTION ( 'NONE',  ( 0.000000000000000000, 0.000000000000000000, -1.000000000000000000 ) ) ;
#15816=ORIENTED_EDGE ( 'NONE', *, *, #14388, .F. ) ;
#15897=DIRECTION ( 'NONE',  ( 0.000000000000000000, -0.000000000000000000, 1.000000000000000000 ) ) ;
#15928=DIRECTION ( 'NONE',  ( -0.000000000000000000, 0.000000000000000000, -1.000000000000000000 ) ) ;
#15933=PRESENTATION_STYLE_ASSIGNMENT (( #19719 ) ) ;
#15958=FACE_OUTER_BOUND ( 'NONE', #10909, .T. ) ;
#15973=CIRCLE ( 'NONE', #6992, 2.500000000000002220 ) ;
#15985=EDGE_CURVE ( 'NONE', #22677, #19900, #2808, .T. ) ;
#16019=AXIS2_PLACEMENT_3D ( 'NONE', #4420, #4542, #1260 ) ;
#16037=AXIS2_PLACEMENT_3D ( 'NONE', #21803, #18381, #2257 ) ;
#16039=CARTESIAN_POINT ( 'NONE',  ( -2.681483223904243207, 3.070647092368421927, 2.148523566439784158E-15 ) ) ;
#16046=CARTESIAN_POINT ( 'NONE',  ( 2.000000000000015543, -3.464101615137746837, -5.600000000000000533 ) ) ;
#16119=DIRECTION ( 'NONE',  ( 1.000000000000000000, 0.000000000000000000, 0.000000000000000000 ) ) ;
#16143=ORIENTED_EDGE ( 'NONE', *, *, #11685, .F. ) ;
#16156=CARTESIAN_POINT ( 'NONE',  ( 0.000000000000000000, 0.000000000000000000, 0.000000000000000000 ) ) ;
#16184=DIRECTION ( 'NONE',  ( -0.000000000000000000, -0.000000000000000000, 1.000000000000000000 ) ) ;
#16207=DIRECTION ( 'NONE',  ( -0.000000000000000000, -0.000000000000000000, 1.000000000000000000 ) ) ;
#16263=CONICAL_SURFACE ( 'NONE', #136, 2.060000000000002718, 0.9599310885968758145 ) ;
#16279=VECTOR ( 'NONE', #12671, 1000.000000000000000 ) ;
#16401=EDGE_CURVE ( 'NONE', #5239, #12423, #12980, .T. ) ;
#16441=DIRECTION ( 'NONE',  ( 1.000000000000000000, 0.000000000000000000, 0.000000000000000000 ) ) ;
#16495=ORIENTED_EDGE ( 'NONE', *, *, #7259, .T. ) ;
#16577=CARTESIAN_POINT ( 'NONE',  ( 0.6543461111163483279, 4.241015250120811153, -5.460849780464857695 ) ) ;
#16605=ADVANCED_FACE ( 'NONE', ( #7137 ), #21530, .T. ) ;
#16677=CIRCLE ( 'NONE', #23092, 4.000000000000000888 ) ;
#16703=DIRECTION ( 'NONE',  ( -0.000000000000000000, -0.000000000000000000, 1.000000000000000000 ) ) ;
#16716=VERTEX_POINT ( 'NONE', #4267 ) ;
#16774=CARTESIAN_POINT ( 'NONE',  ( -4.000000000000003553, 0.000000000000000000, -5.600000000000000533 ) ) ;
#16782=DIRECTION ( 'NONE',  ( 1.000000000000000000, 0.000000000000000000, 0.000000000000000000 ) ) ;
#16797=ORIENTED_EDGE ( 'NONE', *, *, #8765, .T. ) ;
#16805=VERTEX_POINT ( 'NONE', #2859 ) ;
#16822=CIRCLE ( 'NONE', #5593, 3.999999999999999112 ) ;
#16827=ORIENTED_EDGE ( 'NONE', *, *, #11264, .F. ) ;
#16836=EDGE_LOOP ( 'NONE', ( #7287, #16495 ) ) ;
#16843=EDGE_CURVE ( 'NONE', #18558, #9711, #9020, .T. ) ;
#16874=B_SPLINE_CURVE_WITH_KNOTS ( 'NONE', 3,
 ( #2250, #16577, #14835, #2835 ),
 .UNSPECIFIED., .F., .F.,
 ( 4, 4 ),
 ( 2.380737581673561746E-07, 0.002336974151641583314 ),
 .UNSPECIFIED. ) ;
#16879=DIRECTION ( 'NONE',  ( -1.000000000000000000, 0.000000000000000000, 0.000000000000000000 ) ) ;
#16894=ORIENTED_EDGE ( 'NONE', *, *, #11706, .F. ) ;
#16917=EDGE_LOOP ( 'NONE', ( #8053, #16979, #11780, #2268 ) ) ;
#16979=ORIENTED_EDGE ( 'NONE', *, *, #15480, .T. ) ;
#16984=ORIENTED_EDGE ( 'NONE', *, *, #22881, .T. ) ;
#16988=FACE_OUTER_BOUND ( 'NONE', #14626, .T. ) ;
#17019=CARTESIAN_POINT ( 'NONE',  ( 0.000000000000000000, 0.000000000000000000, 0.000000000000000000 ) ) ;
#17091=( LENGTH_UNIT ( ) NAMED_UNIT ( * ) SI_UNIT ( .MILLI., .METRE. ) );
#17106=ADVANCED_FACE ( 'NONE', ( #258 ), #9313, .T. ) ;
#17121=EDGE_CURVE ( 'NONE', #22677, #5239, #16874, .T. ) ;
#17146=FACE_OUTER_BOUND ( 'NONE', #6009, .T. ) ;
#17170=DIRECTION ( 'NONE',  ( 0.000000000000000000, 0.000000000000000000, -1.000000000000000000 ) ) ;
#17189=VERTEX_POINT ( 'NONE', #13887 ) ;
#17214=( NAMED_UNIT ( * ) PLANE_ANGLE_UNIT ( ) SI_UNIT ( $, .RADIAN. ) );
#17265=PLANE ( 'NONE',  #5913 ) ;
#17277=EDGE_CURVE ( 'NONE', #14161, #17189, #6760, .T. ) ;
#17294=ORIENTED_EDGE ( 'NONE', *, *, #23203, .F. ) ;
#17298=ORIENTED_EDGE ( 'NONE', *, *, #22881, .F. ) ;
#17325=( NAMED_UNIT ( * ) SI_UNIT ( $, .STERADIAN. ) SOLID_ANGLE_UNIT ( ) );
#17360=PRODUCT ( 'hex nut gradec_bsi_BS EN 24034 - M5 - N', 'hex nut gradec_bsi_BS EN 24034 - M5 - N', '', ( #3762 ) ) ;
#17361=ORIENTED_EDGE ( 'NONE', *, *, #4244, .T. ) ;
#17363=CARTESIAN_POINT ( 'NONE',  ( -2.000000000000015543, -3.464101615137743728, 0.000000000000000000 ) ) ;
#17379=CARTESIAN_POINT ( 'NONE',  ( -4.000000000000003553, 2.309401076758494487, -5.600000000000000533 ) ) ;
#17389=AXIS2_PLACEMENT_3D ( 'NONE', #6732, #14139, #16119 ) ;
#17461=B_SPLINE_CURVE_WITH_KNOTS ( 'NONE', 3,
 ( #10756, #3130, #1367, #19711, #23006, #19231 ),
 .UNSPECIFIED., .F., .F.,
 ( 4, 2, 4 ),
 ( 0.004120275011746847918, 0.005288420935197131814, 0.006456566858647415710 ),
 .UNSPECIFIED. ) ;
#17465=CARTESIAN_POINT ( 'NONE',  ( 2.678494666091052689, 3.072372537026353267, -5.565789719053469753 ) ) ;
#17518=DIRECTION ( 'NONE',  ( 0.000000000000000000, 0.000000000000000000, -1.000000000000000000 ) ) ;
#17524=CARTESIAN_POINT ( 'NONE',  ( -3.344563996438217224, -2.687817229851500400, -5.441324518471499339 ) ) ;
#17547=CARTESIAN_POINT ( 'NONE',  ( 2.339468227445713033, 3.268109542640643905, 2.462324777668250297E-15 ) ) ;
#17552=ADVANCED_FACE ( 'NONE', ( #4324 ), #8032, .T. ) ;
#17554=DIRECTION ( 'NONE',  ( -1.000000000000000000, 0.000000000000000000, 0.000000000000000000 ) ) ;
#17584=DIRECTION ( 'NONE',  ( -1.000000000000000000, 0.000000000000000000, 0.000000000000000000 ) ) ;
#17589=AXIS2_PLACEMENT_3D ( 'NONE', #850, #8022, #20731 ) ;
#17609=CARTESIAN_POINT ( 'NONE',  ( -2.000000000000015543, 3.464101615137746837, 0.000000000000000000 ) ) ;
#17621=DIRECTION ( 'NONE',  ( 1.000000000000000000, 0.000000000000000000, 0.000000000000000000 ) ) ;
#17669=CARTESIAN_POINT ( 'NONE',  ( 0.000000000000000000, 0.000000000000000000, -5.600000000000000533 ) ) ;
#17732=CARTESIAN_POINT ( 'NONE',  ( 0.000000000000000000, 0.000000000000000000, 0.000000000000000000 ) ) ;
#17764=PRODUCT_DEFINITION_SHAPE ( 'NONE', 'NONE',  #21145 ) ;
#17765=CARTESIAN_POINT ( 'NONE',  ( 4.000000000000003553, -0.7779732554280851531, -0.03354435108168089819 ) ) ;
#17842=CARTESIAN_POINT ( 'NONE',  ( 1.387778780781445676E-14, 4.618802153517020059, -5.242734410091827613 ) ) ;
#17875=EDGE_LOOP ( 'NONE', ( #21266, #421, #23205, #19314 ) ) ;
#17896=ORIENTED_EDGE ( 'NONE', *, *, #15692, .T. ) ;
#17915=CIRCLE ( 'NONE', #19794, 3.999999999999999112 ) ;
#17949=DIRECTION ( 'NONE',  ( 0.000000000000000000, 0.000000000000000000, 1.000000000000000000 ) ) ;
#18032=CARTESIAN_POINT ( 'NONE',  ( 0.000000000000000000, 0.000000000000000000, 0.000000000000000000 ) ) ;
#18041=FACE_OUTER_BOUND ( 'NONE', #21140, .T. ) ;
#18042=ADVANCED_FACE ( 'NONE', ( #5327 ), #2029, .T. ) ;
#18083=LINE ( 'NONE', #1948, #20180 ) ;
#18164=B_SPLINE_CURVE_WITH_KNOTS ( 'NONE', 3,
 ( #2984, #4381, #9930, #18631 ),
 .UNSPECIFIED., .F., .F.,
 ( 4, 4 ),
 ( 2.380737581852663157E-07, 0.002336974151641522165 ),
 .UNSPECIFIED. ) ;
#18258=CARTESIAN_POINT ( 'NONE',  ( 4.000000000000003553, 1.557668341133516599, -5.440303434304243346 ) ) ;
#18279=ADVANCED_FACE ( 'NONE', ( #2367 ), #18581, .T. ) ;
#18283=FACE_OUTER_BOUND ( 'NONE', #12853, .T. ) ;
#18284=EDGE_CURVE ( 'NONE', #9593, #19900, #4460, .T. ) ;
#18297=VERTEX_POINT ( 'NONE', #19183 ) ;
#18298=EDGE_LOOP ( 'NONE', ( #22362, #10001, #3119 ) ) ;
#18318=CARTESIAN_POINT ( 'NONE',  ( -2.500000000000002220, 0.000000000000000000, -5.574599999999999334 ) ) ;
#18366=EDGE_CURVE ( 'NONE', #16716, #902, #9802, .T. ) ;
#18381=DIRECTION ( 'NONE',  ( 0.000000000000000000, 0.000000000000000000, -1.000000000000000000 ) ) ;
#18387=ORIENTED_EDGE ( 'NONE', *, *, #7948, .F. ) ;
#18406=EDGE_CURVE ( 'NONE', #20542, #13382, #15125, .T. ) ;
#18417=ORIENTED_EDGE ( 'NONE', *, *, #18284, .F. ) ;
#18441=VERTEX_POINT ( 'NONE', #7309 ) ;
#18459=AXIS2_PLACEMENT_3D ( 'NONE', #5905, #3597, #17949 ) ;
#18494=ORIENTED_EDGE ( 'NONE', *, *, #2403, .F. ) ;
#18498=EDGE_LOOP ( 'NONE', ( #9799, #6416 ) ) ;
#18518=DIRECTION ( 'NONE',  ( 1.000000000000000000, 0.000000000000000000, 0.000000000000000000 ) ) ;
#18520=VERTEX_POINT ( 'NONE', #3542 ) ;
#18558=VERTEX_POINT ( 'NONE', #1538 ) ;
#18574=ORIENTED_EDGE ( 'NONE', *, *, #6079, .T. ) ;
#18581=CONICAL_SURFACE ( 'NONE', #19654, 4.000000000000000000, 1.047197551196595855 ) ;
#18631=CARTESIAN_POINT ( 'NONE',  ( 2.000000000000015543, -3.464101615137746837, -5.600000000000000533 ) ) ;
#18672=CARTESIAN_POINT ( 'NONE',  ( -4.000000000000003553, 0.3904826640788073289, -5.599999999999998757 ) ) ;
#18674=B_SPLINE_CURVE_WITH_KNOTS ( 'NONE', 3,
 ( #1213, #6615, #22508, #10369, #13562, #20744 ),
 .UNSPECIFIED., .F., .F.,
 ( 4, 2, 4 ),
 ( 0.006456566858647396628, 0.007625406818786647362, 0.008794246778925898095 ),
 .UNSPECIFIED. ) ;
#18682=CARTESIAN_POINT ( 'NONE',  ( 0.000000000000000000, 0.000000000000000000, 0.000000000000000000 ) ) ;
#18688=PLANE ( 'NONE',  #14595 ) ;
#18709=DIRECTION ( 'NONE',  ( 0.000000000000000000, 0.000000000000000000, 1.000000000000000000 ) ) ;
#18715=CARTESIAN_POINT ( 'NONE',  ( -0.3263565795980838957, 4.430380094434251959, -0.2484800633750068877 ) ) ;
#18735=ORIENTED_EDGE ( 'NONE', *, *, #11706, .T. ) ;
#18793=B_SPLINE_CURVE_WITH_KNOTS ( 'NONE', 3,
 ( #21939, #3586, #10866, #5829, #3923, #11217 ),
 .UNSPECIFIED., .F., .F.,
 ( 4, 2, 4 ),
 ( 0.006456566858647415710, 0.007625406818786682923, 0.008794246778925950137 ),
 .UNSPECIFIED. ) ;
#18818=ORIENTED_EDGE ( 'NONE', *, *, #8272, .F. ) ;
#18828=CARTESIAN_POINT ( 'NONE',  ( -4.000000000000003553, 2.309401076758494487, -5.600000000000000533 ) ) ;
#18833=CARTESIAN_POINT ( 'NONE',  ( -2.000000000000015543, 3.464101615137746837, -5.600000000000000533 ) ) ;
#18872=CONICAL_SURFACE ( 'NONE', #22248, 2.500000000000002220, 0.9599310885968830309 ) ;
#18922=EDGE_CURVE ( 'NONE', #16805, #7255, #14777, .T. ) ;
#18935=LINE ( 'NONE', #22463, #7376 ) ;
#18990=CARTESIAN_POINT ( 'NONE',  ( -4.000000000000002665, -0.7779732554280794909, -0.03354435108168014879 ) ) ;
#18997=ORIENTED_EDGE ( 'NONE', *, *, #9645, .T. ) ;
#19042=EDGE_CURVE ( 'NONE', #12423, #9711, #7502, .T. ) ;
#19114=ORIENTED_EDGE ( 'NONE', *, *, #19042, .F. ) ;
#19123=AXIS2_PLACEMENT_3D ( 'NONE', #18032, #14147, #21226 ) ;
#19125=AXIS2_PLACEMENT_3D ( 'NONE', #15591, #22781, #6656 ) ;
#19152=PRODUCT_DEFINITION_FORMATION_WITH_SPECIFIED_SOURCE ( 'ANY', '', #17360, .NOT_KNOWN. ) ;
#19166=ORIENTED_EDGE ( 'NONE', *, *, #912, .T. ) ;
#19183=CARTESIAN_POINT ( 'NONE',  ( -2.099999999999999645, 2.571758278209440971E-16, -5.294516984716112873 ) ) ;
#19231=CARTESIAN_POINT ( 'NONE',  ( 4.000000000000003553, 0.000000000000000000, -5.600000000000000533 ) ) ;
#19314=ORIENTED_EDGE ( 'NONE', *, *, #1345, .F. ) ;
#19316=EDGE_LOOP ( 'NONE', ( #3188, #3265, #18417 ) ) ;
#19328=CARTESIAN_POINT ( 'NONE',  ( -2.099999999999999645, 2.571758278209440971E-16, -5.600000000000000533 ) ) ;
#19384=LINE ( 'NONE', #1849, #13418 ) ;
#19465=AXIS2_PLACEMENT_3D ( 'NONE', #2778, #20547, #13368 ) ;
#19637=CARTESIAN_POINT ( 'NONE',  ( 0.000000000000000000, 0.000000000000000000, -5.574599999999999334 ) ) ;
#19638=EDGE_CURVE ( 'NONE', #4023, #1072, #16677, .T. ) ;
#19642=ORIENTED_EDGE ( 'NONE', *, *, #15985, .F. ) ;
#19654=AXIS2_PLACEMENT_3D ( 'NONE', #9660, #16703, #11193 ) ;
#19711=CARTESIAN_POINT ( 'NONE',  ( 4.000000000000004441, -0.7779732554280850421, -5.566455648918319454 ) ) ;
#19719=SURFACE_STYLE_USAGE ( .BOTH. , #7142 ) ;
#19762=EDGE_CURVE ( 'NONE', #13382, #22677, #14823, .T. ) ;
#19794=AXIS2_PLACEMENT_3D ( 'NONE', #17019, #11854, #9983 ) ;
#19830=CIRCLE ( 'NONE', #7438, 4.000000000000000000 ) ;
#19864=ORIENTED_EDGE ( 'NONE', *, *, #17121, .T. ) ;
#19900=VERTEX_POINT ( 'NONE', #20956 ) ;
#19954=ORIENTED_EDGE ( 'NONE', *, *, #16401, .T. ) ;
#20029=CARTESIAN_POINT ( 'NONE',  ( 0.3263565795980739592, -4.430380094434307026, -5.351519936624962170 ) ) ;
#20102=CARTESIAN_POINT ( 'NONE',  ( -6.938893903907228378E-14, -4.618802153517020059, -5.242734410091827613 ) ) ;
#20145=CARTESIAN_POINT ( 'NONE',  ( 0.000000000000000000, 0.000000000000000000, -5.294516984716112873 ) ) ;
#20175=CARTESIAN_POINT ( 'NONE',  ( 2.000000000000029310, 3.464101615137740175, -5.600000000000000533 ) ) ;
#20180=VECTOR ( 'NONE', #14863, 1000.000000000000000 ) ;
#20222=VERTEX_POINT ( 'NONE', #11623 ) ;
#20234=CARTESIAN_POINT ( 'NONE',  ( 0.000000000000000000, -4.618802153517061804, -5.600000000000000533 ) ) ;
#20262=CARTESIAN_POINT ( 'NONE',  ( 4.000000000000003553, 0.000000000000000000, -5.600000000000000533 ) ) ;
#20277=ORIENTED_EDGE ( 'NONE', *, *, #18366, .F. ) ;
#20332=CARTESIAN_POINT ( 'NONE',  ( -4.000000000000003553, -2.309401076758532678, -5.242734410091827613 ) ) ;
#20359=ORIENTED_EDGE ( 'NONE', *, *, #3079, .T. ) ;
#20386=ORIENTED_EDGE ( 'NONE', *, *, #1080, .F. ) ;
#20401=ADVANCED_FACE ( 'NONE', ( #15958 ), #21632, .T. ) ;
#20420=ORIENTED_EDGE ( 'NONE', *, *, #19762, .T. ) ;
#20443=CARTESIAN_POINT ( 'NONE',  ( -2.678494666091062459, -3.072372537026391459, -0.03421028094655022972 ) ) ;
#20463=DIRECTION ( 'NONE',  ( 0.000000000000000000, 0.000000000000000000, 1.000000000000000000 ) ) ;
#20512=VERTEX_POINT ( 'NONE', #18318 ) ;
#20542=VERTEX_POINT ( 'NONE', #14787 ) ;
#20547=DIRECTION ( 'NONE',  ( 0.000000000000000000, 0.000000000000000000, 1.000000000000000000 ) ) ;
#20593=AXIS2_PLACEMENT_3D ( 'NONE', #9286, #12929, #2333 ) ;
#20623=ORIENTED_EDGE ( 'NONE', *, *, #1345, .T. ) ;
#20673=MANIFOLD_SOLID_BREP ( 'EndChamfer', #12936 ) ;
#20687=CARTESIAN_POINT ( 'NONE',  ( -4.000000000000003553, 1.557668341133521483, -5.440303434304241570 ) ) ;
#20731=DIRECTION ( 'NONE',  ( -1.000000000000000000, 3.552713678800500929E-15, 0.000000000000000000 ) ) ;
#20744=CARTESIAN_POINT ( 'NONE',  ( -4.000000000000003553, 2.309401076758494487, -0.3572655899081629283 ) ) ;
#20783=ADVANCED_FACE ( 'NONE', ( #4014 ), #4127, .F. ) ;
#20830=DIRECTION ( 'NONE',  ( 0.000000000000000000, 0.000000000000000000, 1.000000000000000000 ) ) ;
#20868=DIRECTION ( 'NONE',  ( 1.000000000000000000, 0.000000000000000000, 0.000000000000000000 ) ) ;
#20896=CARTESIAN_POINT ( 'NONE',  ( 3.673643420401899728, 2.497823135841254150, -5.351519936625005691 ) ) ;
#20902=FILL_AREA_STYLE_COLOUR ( '', #22590 ) ;
#20950=DIRECTION ( 'NONE',  ( 1.000000000000000000, 0.000000000000000000, 0.000000000000000000 ) ) ;
#20956=CARTESIAN_POINT ( 'NONE',  ( 1.387778780781445676E-14, 4.618802153517020059, -0.3572655899081733644 ) ) ;
#20984=CONICAL_SURFACE ( 'NONE', #2551, 2.500000000000002220, 0.9599310885968830309 ) ;
#21002=EDGE_LOOP ( 'NONE', ( #8116, #6668, #16984, #8296 ) ) ;
#21025=AXIS2_PLACEMENT_3D ( 'NONE', #7405, #21762, #16441 ) ;
#21030=ORIENTED_EDGE ( 'NONE', *, *, #15692, .F. ) ;
#21036=CARTESIAN_POINT ( 'NONE',  ( 2.681483223904249424, -3.070647092368467668, -2.185966214620738111E-14 ) ) ;
#21079=ORIENTED_EDGE ( 'NONE', *, *, #8765, .F. ) ;
#21098=CARTESIAN_POINT ( 'NONE',  ( 0.6554360035617851077, -4.240386000424089197, -0.1586754815285195408 ) ) ;
#21122=FACE_OUTER_BOUND ( 'NONE', #9625, .T. ) ;
#21140=EDGE_LOOP ( 'NONE', ( #18494, #14229, #12857 ) ) ;
#21145=PRODUCT_DEFINITION ( 'UNKNOWN', '', #19152, #22524 ) ;
#21175=CIRCLE ( 'NONE', #11014, 4.000000000000000888 ) ;
#21193=CARTESIAN_POINT ( 'NONE',  ( 4.000000000000003553, 0.000000000000000000, 0.000000000000000000 ) ) ;
#21205=EDGE_CURVE ( 'NONE', #7463, #5232, #18935, .T. ) ;
#21217=DIRECTION ( 'NONE',  ( -1.000000000000000000, 0.000000000000000000, 0.000000000000000000 ) ) ;
#21226=DIRECTION ( 'NONE',  ( -1.000000000000000000, 0.000000000000000000, 0.000000000000000000 ) ) ;
#21266=ORIENTED_EDGE ( 'NONE', *, *, #7259, .F. ) ;
#21275=FACE_OUTER_BOUND ( 'NONE', #9367, .T. ) ;
#21278=DIRECTION ( 'NONE',  ( -1.000000000000000000, 0.000000000000000000, 0.000000000000000000 ) ) ;
#21296=B_SPLINE_CURVE_WITH_KNOTS ( 'NONE', 3,
 ( #3047, #6461, #22352, #2929 ),
 .UNSPECIFIED., .F., .F.,
 ( 4, 4 ),
 ( 2.380737581673407957E-07, 0.002336974151641583747 ),
 .UNSPECIFIED. ) ;
#21299=CARTESIAN_POINT ( 'NONE',  ( 0.000000000000000000, 0.000000000000000000, 0.000000000000000000 ) ) ;
#21340=CARTESIAN_POINT ( 'NONE',  ( 0.000000000000000000, 0.000000000000000000, -5.600000000000000533 ) ) ;
#21344=FACE_OUTER_BOUND ( 'NONE', #21002, .T. ) ;
#21377=CIRCLE ( 'NONE', #11208, 4.000000000000000888 ) ;
#21420=VECTOR ( 'NONE', #11039, 1000.000000000000000 ) ;
#21426=CARTESIAN_POINT ( 'NONE',  ( -2.000000000000015543, 3.464101615137746837, -5.600000000000000533 ) ) ;
#21435=DIRECTION ( 'NONE',  ( -1.000000000000000000, 0.000000000000000000, 0.000000000000000000 ) ) ;
#21442=EDGE_LOOP ( 'NONE', ( #20420, #19864, #18735 ) ) ;
#21470=EDGE_CURVE ( 'NONE', #7255, #16805, #625, .T. ) ;
#21530=CONICAL_SURFACE ( 'NONE', #6488, 4.000000000000000000, 1.047197551196595855 ) ;
#21554=CIRCLE ( 'NONE', #6882, 4.000000000000000888 ) ;
#21574=APPLICATION_CONTEXT ( 'automotive_design' ) ;
#21589=VERTEX_POINT ( 'NONE', #796 ) ;
#21597=DIRECTION ( 'NONE',  ( 0.000000000000000000, 0.000000000000000000, -1.000000000000000000 ) ) ;
#21632=CONICAL_SURFACE ( 'NONE', #1704, 4.000000000000000000, 1.047197551196595855 ) ;
#21681=DIRECTION ( 'NONE',  ( -1.000000000000000000, 1.776356839400250465E-15, 0.000000000000000000 ) ) ;
#21703=ORIENTED_EDGE ( 'NONE', *, *, #17121, .F. ) ;
#21736=CONICAL_SURFACE ( 'NONE', #14591, 4.000000000000000000, 1.047197551196595855 ) ;
#21762=DIRECTION ( 'NONE',  ( -0.000000000000000000, -0.000000000000000000, 1.000000000000000000 ) ) ;
#21803=CARTESIAN_POINT ( 'NONE',  ( 0.000000000000000000, 0.000000000000000000, 0.000000000000000000 ) ) ;
#21834=ORIENTED_EDGE ( 'NONE', *, *, #16401, .F. ) ;
#21874=VECTOR ( 'NONE', #9890, 1000.000000000000000 ) ;
#21885=EDGE_LOOP ( 'NONE', ( #4309, #10834, #20386, #18387, #5313, #15793 ) ) ;
#21902=CARTESIAN_POINT ( 'NONE',  ( -1.321505333908965962, 3.855830693249139962, -5.565789719053468865 ) ) ;
#21924=ORIENTED_EDGE ( 'NONE', *, *, #19638, .F. ) ;
#21939=CARTESIAN_POINT ( 'NONE',  ( 4.000000000000003553, 0.000000000000000000, 0.000000000000000000 ) ) ;
#22018=CARTESIAN_POINT ( 'NONE',  ( 0.6554360035617849967, -4.240386000424089197, -5.441324518471480687 ) ) ;
#22115=AXIS2_PLACEMENT_3D ( 'NONE', #4943, #2963, #5306 ) ;
#22122=ORIENTED_EDGE ( 'NONE', *, *, #18366, .T. ) ;
#22140=COLOUR_RGB ( '', 0.08235294, 0.09019608, 0.10196078) ;
#22198=CARTESIAN_POINT ( 'NONE',  ( 4.000000000000003553, 2.309401076758480720, -5.600000000000000533 ) ) ;
#22248=AXIS2_PLACEMENT_3D ( 'NONE', #5684, #10733, #14614 ) ;
#22250=CARTESIAN_POINT ( 'NONE',  ( -1.660531772554314722, 3.660093687634845772, 3.346627174601739456E-15 ) ) ;
#22266=B_SPLINE_CURVE_WITH_KNOTS ( 'NONE', 3,
 ( #20262, #3780, #23135, #18258, #3373, #7775 ),
 .UNSPECIFIED., .F., .F.,
 ( 4, 2, 4 ),
 ( 0.006456566858647415710, 0.007625406818786682923, 0.008794246778925950137 ),
 .UNSPECIFIED. ) ;
#22291=( LENGTH_UNIT ( ) NAMED_UNIT ( * ) SI_UNIT ( .MILLI., .METRE. ) );
#22330=ORIENTED_EDGE ( 'NONE', *, *, #9516, .F. ) ;
#22352=CARTESIAN_POINT ( 'NONE',  ( 1.318516776095790322, 3.857556137907070859, 2.806962664615227643E-15 ) ) ;
#22362=ORIENTED_EDGE ( 'NONE', *, *, #8682, .F. ) ;
#22393=ORIENTED_EDGE ( 'NONE', *, *, #19042, .T. ) ;
#22463=CARTESIAN_POINT ( 'NONE',  ( 2.500000000000002220, 3.061616997868386099E-16, -5.574599999999999334 ) ) ;
#22464=AXIS2_PLACEMENT_3D ( 'NONE', #14986, #2052, #18518 ) ;
#22508=CARTESIAN_POINT ( 'NONE',  ( -4.000000000000004441, 0.7862748000878052590, -0.03447227762756794461 ) ) ;
#22524=PRODUCT_DEFINITION_CONTEXT ( 'detailed design', #21574, 'design' ) ;
#22526=FILL_AREA_STYLE_COLOUR ( '', #22140 ) ;
#22574=LINE ( 'NONE', #7991, #10045 ) ;
#22590=COLOUR_RGB ( '', 0.08235294, 0.09019608, 0.10196078) ;
#22675=DIRECTION ( 'NONE',  ( 0.000000000000000000, 0.000000000000000000, 1.000000000000000000 ) ) ;
#22677=VERTEX_POINT ( 'NONE', #17842 ) ;
#22781=DIRECTION ( 'NONE',  ( 0.5000000000000066613, 0.8660254037844348218, -0.000000000000000000 ) ) ;
#22839=CARTESIAN_POINT ( 'NONE',  ( -2.681483223904238322, 3.070647092368425479, -5.600000000000002309 ) ) ;
#22865=AXIS2_PLACEMENT_3D ( 'NONE', #14350, #10820, #21435 ) ;
#22875=EDGE_CURVE ( 'NONE', #1072, #5239, #19830, .T. ) ;
#22881=EDGE_CURVE ( 'NONE', #18297, #20512, #10738, .T. ) ;
#22913=ORIENTED_EDGE ( 'NONE', *, *, #17277, .T. ) ;
#22950=DIRECTION ( 'NONE',  ( -0.000000000000000000, -0.000000000000000000, 1.000000000000000000 ) ) ;
#22995=ORIENTED_EDGE ( 'NONE', *, *, #18284, .T. ) ;
#23004=CARTESIAN_POINT ( 'NONE',  ( 3.344563996438205677, 2.687817229851463985, -5.441324518471517102 ) ) ;
#23006=CARTESIAN_POINT ( 'NONE',  ( 4.000000000000003553, -0.3902508023145571658, -5.599999999999998757 ) ) ;
#23035=CARTESIAN_POINT ( 'NONE',  ( -2.099999999999999645, 2.571758278209440971E-16, -0.2800830152838856835 ) ) ;
#23092=AXIS2_PLACEMENT_3D ( 'NONE', #21340, #15897, #21681 ) ;
#23107=CARTESIAN_POINT ( 'NONE',  ( 1.321505333908973956, -3.855830693249185259, -0.03421028094655655799 ) ) ;
#23135=CARTESIAN_POINT ( 'NONE',  ( 4.000000000000004441, 0.7862748000878162502, -5.565527722372433317 ) ) ;
#23164=DIRECTION ( 'NONE',  ( 0.000000000000000000, 0.000000000000000000, -1.000000000000000000 ) ) ;
#23190=CARTESIAN_POINT ( 'NONE',  ( 3.999999999999989786, -2.309401076758549998, -0.3572655899081733644 ) ) ;
#23203=EDGE_CURVE ( 'NONE', #13382, #6061, #6332, .T. ) ;
#23205=ORIENTED_EDGE ( 'NONE', *, *, #2180, .T. ) ;
#23227=EDGE_CURVE ( 'NONE', #6061, #16716, #21377, .T. ) ;
ENDSEC;
END-ISO-10303-21;
